ISO-10303-21;
HEADER;
FILE_DESCRIPTION (('STEP AP214'),
    '1' );
FILE_NAME ('Housing.step',
    '2026-10-24T18:16:00',
    ( '' ),
    ( '' ),
    'SwSTEP 2.0',
    'SolidWorks 2025',
    '' );
FILE_SCHEMA (( 'AUTOMOTIVE_DESIGN' ));
ENDSEC;

DATA;
#3=DIRECTION ( 'NONE',  ( 0.000000000000000000, 1.000000000000000000, 0.000000000000000000 ) ) ;
#10=DIRECTION ( 'NONE',  ( -1.000000000000000000, 0.000000000000000000, 0.000000000000000000 ) ) ;
#17=ORIENTED_EDGE ( 'NONE', *, *, #14890, .T. ) ;
#25=VERTEX_POINT ( 'NONE', #9568 ) ;
#28=DIRECTION ( 'NONE',  ( 1.000000000000000000, 0.000000000000000000, 0.000000000000000000 ) ) ;
#30=CARTESIAN_POINT ( 'NONE',  ( -0.7455328141524870667, 1.338582677165354395, 0.3622425942647020669 ) ) ;
#36=EDGE_CURVE ( 'NONE', #8997, #3695, #14891, .T. ) ;
#45=CARTESIAN_POINT ( 'NONE',  ( -0.05905511811023625435, 2.637795275590551825, 0.03937007874015747977 ) ) ;
#53=EDGE_CURVE ( 'NONE', #7634, #4333, #7363, .T. ) ;
#65=CARTESIAN_POINT ( 'NONE',  ( 0.000000000000000000, 0.5511811023622046335, 0.5590551181102362266 ) ) ;
#67=DIRECTION ( 'NONE',  ( -0.000000000000000000, -1.000000000000000000, -0.000000000000000000 ) ) ;
#68=ORIENTED_EDGE ( 'NONE', *, *, #14092, .T. ) ;
#71=DIRECTION ( 'NONE',  ( 0.000000000000000000, 0.000000000000000000, 1.000000000000000000 ) ) ;
#76=ORIENTED_EDGE ( 'NONE', *, *, #1408, .T. ) ;
#81=CARTESIAN_POINT ( 'NONE',  ( 6.750021727583836750E-17, 1.409448818897637956, 0.5511811023622046335 ) ) ;
#84=DIRECTION ( 'NONE',  ( 0.000000000000000000, 0.000000000000000000, 1.000000000000000000 ) ) ;
#91=ORIENTED_EDGE ( 'NONE', *, *, #2937, .F. ) ;
#95=CARTESIAN_POINT ( 'NONE',  ( 0.000000000000000000, 0.3543307086614172485, 0.000000000000000000 ) ) ;
#96=CARTESIAN_POINT ( 'NONE',  ( 0.000000000000000000, 0.000000000000000000, 0.000000000000000000 ) ) ;
#103=CIRCLE ( 'NONE', #4332, 0.5905511811023621549 ) ;
#112=CIRCLE ( 'NONE', #12619, 0.007874015748031449116 ) ;
#115=VERTEX_POINT ( 'NONE', #10106 ) ;
#116=EDGE_CURVE ( 'NONE', #14687, #9581, #13722, .T. ) ;
#121=DIRECTION ( 'NONE',  ( 0.000000000000000000, 0.000000000000000000, 1.000000000000000000 ) ) ;
#123=DIRECTION ( 'NONE',  ( -0.000000000000000000, -1.000000000000000000, -0.000000000000000000 ) ) ;
#124=LINE ( 'NONE', #4886, #11098 ) ;
#127=FACE_OUTER_BOUND ( 'NONE', #1547, .T. ) ;
#129=DIRECTION ( 'NONE',  ( 1.224646799147343593E-16, 0.000000000000000000, -1.000000000000000000 ) ) ;
#135=CARTESIAN_POINT ( 'NONE',  ( 0.000000000000000000, 1.661417322834646049, 0.000000000000000000 ) ) ;
#147=DIRECTION ( 'NONE',  ( -1.000000000000000000, -0.000000000000000000, -0.000000000000000000 ) ) ;
#151=EDGE_CURVE ( 'NONE', #15270, #8791, #5117, .T. ) ;
#157=CARTESIAN_POINT ( 'NONE',  ( -0.1181102362204724532, 2.637795275590551825, 0.03937007874015747977 ) ) ;
#158=AXIS2_PLACEMENT_3D ( 'NONE', #7725, #15171, #6528 ) ;
#160=AXIS2_PLACEMENT_3D ( 'NONE', #13660, #12490, #1985 ) ;
#163=AXIS2_PLACEMENT_3D ( 'NONE', #230, #8581, #13368 ) ;
#170=DIRECTION ( 'NONE',  ( 0.8660254037844361541, 0.000000000000000000, -0.5000000000000042188 ) ) ;
#173=PLANE ( 'NONE',  #1826 ) ;
#174=CARTESIAN_POINT ( 'NONE',  ( 0.06012952712669449029, 1.041728495490239714, -0.5902914708161598467 ) ) ;
#177=ORIENTED_EDGE ( 'NONE', *, *, #4532, .F. ) ;
#179=DIRECTION ( 'NONE',  ( 0.000000000000000000, -1.000000000000000000, -0.000000000000000000 ) ) ;
#180=CARTESIAN_POINT ( 'NONE',  ( 0.5412478373021326616, 1.346456692913385877, 0.2362233606508025163 ) ) ;
#184=VECTOR ( 'NONE', #3800, 39.37007874015748143 ) ;
#185=ORIENTED_EDGE ( 'NONE', *, *, #10784, .F. ) ;
#186=AXIS2_PLACEMENT_3D ( 'NONE', #15359, #11769, #5780 ) ;
#190=CARTESIAN_POINT ( 'NONE',  ( -0.05905511811023622659, 1.043263280880422528, -0.5946706712680680518 ) ) ;
#195=DIRECTION ( 'NONE',  ( 0.000000000000000000, 0.000000000000000000, 1.000000000000000000 ) ) ;
#201=DIRECTION ( 'NONE',  ( 0.000000000000000000, 1.000000000000000000, -4.956352788505160310E-16 ) ) ;
#204=ORIENTED_EDGE ( 'NONE', *, *, #11325, .F. ) ;
#205=ORIENTED_EDGE ( 'NONE', *, *, #2078, .T. ) ;
#208=DIRECTION ( 'NONE',  ( 0.000000000000000000, 0.000000000000000000, 1.000000000000000000 ) ) ;
#209=AXIS2_PLACEMENT_3D ( 'NONE', #893, #5803, #3406 ) ;
#211=CARTESIAN_POINT ( 'NONE',  ( 0.000000000000000000, 0.007874015748031480341, 0.000000000000000000 ) ) ;
#213=LENGTH_MEASURE_WITH_UNIT ( LENGTH_MEASURE( 0.02539999999999999897 ), #11062 );
#219=FACE_OUTER_BOUND ( 'NONE', #2008, .T. ) ;
#220=VECTOR ( 'NONE', #11691, 39.37007874015748143 ) ;
#226=PLANE ( 'NONE',  #15109 ) ;
#228=VECTOR ( 'NONE', #10852, 39.37007874015748854 ) ;
#230=CARTESIAN_POINT ( 'NONE',  ( 0.000000000000000000, 1.622047244094488638, 0.000000000000000000 ) ) ;
#231=CARTESIAN_POINT ( 'NONE',  ( 0.000000000000000000, 1.035433070866142113, 0.000000000000000000 ) ) ;
#232=DIRECTION ( 'NONE',  ( 0.000000000000000000, 0.000000000000000000, 1.000000000000000000 ) ) ;
#233=CARTESIAN_POINT ( 'NONE',  ( 0.05905511811023622659, 1.338626482899105241, -0.5946706712680680518 ) ) ;
#237=ORIENTED_EDGE ( 'NONE', *, *, #13998, .T. ) ;
#239=ORIENTED_EDGE ( 'NONE', *, *, #11299, .T. ) ;
#240=ADVANCED_FACE ( 'NONE', ( #9406, #9315 ), #14182, .F. ) ;
#249=DIRECTION ( 'NONE',  ( 0.000000000000000000, 0.000000000000000000, 1.000000000000000000 ) ) ;
#252=EDGE_CURVE ( 'NONE', #9167, #12754, #13947, .T. ) ;
#255=ADVANCED_FACE ( 'NONE', ( #3218 ), #9172, .F. ) ;
#257=ORIENTED_EDGE ( 'NONE', *, *, #3314, .T. ) ;
#259=FACE_OUTER_BOUND ( 'NONE', #15085, .T. ) ;
#260=EDGE_CURVE ( 'NONE', #5799, #11532, #7989, .T. ) ;
#267=DIRECTION ( 'NONE',  ( -0.000000000000000000, -1.000000000000000000, -0.000000000000000000 ) ) ;
#276=EDGE_CURVE ( 'NONE', #15338, #8722, #1320, .T. ) ;
#288=VERTEX_POINT ( 'NONE', #4991 ) ;
#295=PLANE ( 'NONE',  #11664 ) ;
#300=ORIENTED_EDGE ( 'NONE', *, *, #2278, .F. ) ;
#304=ORIENTED_EDGE ( 'NONE', *, *, #14593, .F. ) ;
#309=PRODUCT ( 'Housing', 'Housing', '', ( #13499 ) ) ;
#312=CARTESIAN_POINT ( 'NONE',  ( 0.000000000000000000, 1.370078740157480546, 0.000000000000000000 ) ) ;
#323=ADVANCED_FACE ( 'NONE', ( #13159, #11998 ), #8458, .F. ) ;
#325=CARTESIAN_POINT ( 'NONE',  ( 0.7455328141524921737, 1.190944881889763884, 0.3622425942646917418 ) ) ;
#326=CYLINDRICAL_SURFACE ( 'NONE', #8227, 0.007874015748031516770 ) ;
#327=DIRECTION ( 'NONE',  ( 0.000000000000000000, -0.000000000000000000, 1.000000000000000000 ) ) ;
#328=ORIENTED_EDGE ( 'NONE', *, *, #10975, .T. ) ;
#337=EDGE_LOOP ( 'NONE', ( #12113, #13474, #4533, #12286 ) ) ;
#343=CIRCLE ( 'NONE', #10844, 0.03937007874015761855 ) ;
#346=DIRECTION ( 'NONE',  ( 0.000000000000000000, 1.000000000000000000, 0.000000000000000000 ) ) ;
#350=DIRECTION ( 'NONE',  ( -0.000000000000000000, -1.000000000000000000, -0.000000000000000000 ) ) ;
#354=DIRECTION ( 'NONE',  ( 0.000000000000000000, 1.000000000000000000, -4.956352788505160310E-16 ) ) ;
#355=AXIS2_PLACEMENT_3D ( 'NONE', #3021, #14778, #12973 ) ;
#363=ORIENTED_EDGE ( 'NONE', *, *, #11002, .F. ) ;
#364=DIRECTION ( 'NONE',  ( -1.000000000000000000, 0.000000000000000000, 0.000000000000000000 ) ) ;
#366=CIRCLE ( 'NONE', #3856, 0.5984251968503937480 ) ;
#375=CARTESIAN_POINT ( 'NONE',  ( 0.000000000000000000, 1.653543307086614567, 0.000000000000000000 ) ) ;
#376=DIRECTION ( 'NONE',  ( 0.4999999999999919509, -0.000000000000000000, -0.8660254037844432595 ) ) ;
#377=ORIENTED_EDGE ( 'NONE', *, *, #13177, .T. ) ;
#378=EDGE_CURVE ( 'NONE', #10793, #6772, #12896, .T. ) ;
#380=VECTOR ( 'NONE', #667, 39.37007874015747433 ) ;
#381=VERTEX_POINT ( 'NONE', #13298 ) ;
#394=CARTESIAN_POINT ( 'NONE',  ( 0.06604848736013260724, 1.035433070866141891, -0.5868460571724354313 ) ) ;
#395=AXIS2_PLACEMENT_3D ( 'NONE', #14678, #11510, #3210 ) ;
#401=FACE_OUTER_BOUND ( 'NONE', #9524, .T. ) ;
#407=AXIS2_PLACEMENT_3D ( 'NONE', #14638, #376, #9781 ) ;
#411=DIRECTION ( 'NONE',  ( -1.000000000000000000, 4.292327424963333000E-16, -5.289613918360294193E-33 ) ) ;
#416=CARTESIAN_POINT ( 'NONE',  ( 0.000000000000000000, 0.5984251968503937480, 0.000000000000000000 ) ) ;
#419=CIRCLE ( 'NONE', #3163, 0.5984251968503937480 ) ;
#424=EDGE_CURVE ( 'NONE', #1254, #2210, #5620, .T. ) ;
#430=CARTESIAN_POINT ( 'NONE',  ( 0.4854723491485768982, 1.043263280880422528, 0.3484785681409844904 ) ) ;
#433=DIRECTION ( 'NONE',  ( 0.000000000000000000, 0.000000000000000000, -1.000000000000000000 ) ) ;
#440=AXIS2_PLACEMENT_3D ( 'NONE', #4329, #9129, #13902 ) ;
#443=DIRECTION ( 'NONE',  ( 0.000000000000000000, 0.000000000000000000, -1.000000000000000000 ) ) ;
#447=EDGE_CURVE ( 'NONE', #12889, #4456, #881, .T. ) ;
#449=DIRECTION ( 'NONE',  ( -1.000000000000000000, 0.000000000000000000, 0.000000000000000000 ) ) ;
#450=VERTEX_POINT ( 'NONE', #14958 ) ;
#458=CIRCLE ( 'NONE', #15208, 0.1476377952755906220 ) ;
#468=ORIENTED_EDGE ( 'NONE', *, *, #9328, .F. ) ;
#473=EDGE_LOOP ( 'NONE', ( #12721, #4306, #12008, #8418 ) ) ;
#477=DIRECTION ( 'NONE',  ( 0.000000000000000000, 0.000000000000000000, -1.000000000000000000 ) ) ;
#479=ADVANCED_FACE ( 'NONE', ( #6538 ), #4638, .T. ) ;
#480=CARTESIAN_POINT ( 'NONE',  ( 0.000000000000000000, 0.000000000000000000, 0.000000000000000000 ) ) ;
#481=DIRECTION ( 'NONE',  ( 0.000000000000000000, 0.000000000000000000, 1.000000000000000000 ) ) ;
#482=VECTOR ( 'NONE', #10408, 39.37007874015748854 ) ;
#490=CARTESIAN_POINT ( 'NONE',  ( 0.000000000000000000, 1.035433070866142113, 0.000000000000000000 ) ) ;
#497=CARTESIAN_POINT ( 'NONE',  ( 0.000000000000000000, 0.3228346456692913757, 0.000000000000000000 ) ) ;
#499=CARTESIAN_POINT ( 'NONE',  ( -0.5445274672588088505, 1.043263280880422528, 0.2461921031270815630 ) ) ;
#503=CARTESIAN_POINT ( 'NONE',  ( 0.000000000000000000, 0.03937007874015749365, 0.000000000000000000 ) ) ;
#513=EDGE_CURVE ( 'NONE', #14143, #14454, #5809, .T. ) ;
#523=DIRECTION ( 'NONE',  ( -1.224646799147343593E-16, 0.000000000000000000, -1.000000000000000000 ) ) ;
#528=FACE_OUTER_BOUND ( 'NONE', #10014, .T. ) ;
#529=EDGE_CURVE ( 'NONE', #9431, #11432, #639, .T. ) ;
#535=DIRECTION ( 'NONE',  ( 0.000000000000000000, 1.000000000000000000, 0.000000000000000000 ) ) ;
#536=DIRECTION ( 'NONE',  ( 0.000000000000000000, 0.000000000000000000, 1.000000000000000000 ) ) ;
#541=CARTESIAN_POINT ( 'NONE',  ( 0.000000000000000000, 1.653543307086614567, 0.000000000000000000 ) ) ;
#545=CARTESIAN_POINT ( 'NONE',  ( 0.000000000000000000, 2.433070866141732846, 0.000000000000000000 ) ) ;
#547=CARTESIAN_POINT ( 'NONE',  ( 0.000000000000000000, 0.007874015748031480341, 0.000000000000000000 ) ) ;
#558=PLANE ( 'NONE',  #8104 ) ;
#560=EDGE_LOOP ( 'NONE', ( #8023, #12379, #10629, #7056 ) ) ;
#562=VERTEX_POINT ( 'NONE', #13772 ) ;
#563=VERTEX_POINT ( 'NONE', #1859 ) ;
#571=TOROIDAL_SURFACE ( 'NONE', #3323, 0.5826771653543306728, 0.007874015748031495954 ) ;
#575=CARTESIAN_POINT ( 'NONE',  ( 0.000000000000000000, 0.3543307086614172485, 0.000000000000000000 ) ) ;
#578=ORIENTED_EDGE ( 'NONE', *, *, #12657, .F. ) ;
#582=CIRCLE ( 'NONE', #1333, 0.6614173228346456046 ) ;
#592=CARTESIAN_POINT ( 'NONE',  ( -0.6864776960422505070, 1.190944881889763884, 0.4645290592786119332 ) ) ;
#595=DIRECTION ( 'NONE',  ( -0.000000000000000000, -1.000000000000000000, -0.000000000000000000 ) ) ;
#597=AXIS2_PLACEMENT_3D ( 'NONE', #5978, #13115, #6042 ) ;
#598=LINE ( 'NONE', #8911, #2398 ) ;
#603=AXIS2_PLACEMENT_3D ( 'NONE', #3145, #649, #11524 ) ;
#604=ORIENTED_EDGE ( 'NONE', *, *, #2251, .F. ) ;
#607=ORIENTED_EDGE ( 'NONE', *, *, #5187, .F. ) ;
#615=CARTESIAN_POINT ( 'NONE',  ( 0.000000000000000000, 0.03149606299212599769, 0.000000000000000000 ) ) ;
#622=DIRECTION ( 'NONE',  ( 0.000000000000000000, 4.625929269271485914E-16, 1.000000000000000000 ) ) ;
#630=CLOSED_SHELL ( 'NONE', ( #2826, #6462, #11219, #7557, #8656, #6333, #11542, #4063, #2496, #479, #2527, #9426, #8002, #10340, #3553, #6967, #11921, #6795, #12781, #8537, #1463, #14636, #10299, #12107, #1955, #8483, #10469, #12014, #3014, #10797, #6410, #14699, #14590, #6732, #3320, #12442, #14003, #12202, #11073, #4226, #4468, #3024, #12714, #323, #5299, #9071, #15352, #14777, #10707, #10079, #2785, #13450, #255, #1758, #5659, #12783, #804, #14280, #240, #4507, #7067, #7800, #1378, #3486, #15166, #13336, #7438, #10402, #5977, #4755, #6226, #6125, #9312, #6311, #14243, #11262, #13908, #4731, #14706, #2149, #8957, #7135, #9243, #2881, #1285, #782, #13569, #13309, #6620, #4328, #9213, #5137, #11306, #11414, #10561, #12145, #6624, #3998, #9656, #10949, #9814, #13645, #12298, #7765, #4804, #7297, #8589, #2790, #14496, #7979, #5078, #14559, #6034, #11241, #3602, #3215, #2808, #15273, #3107, #13527, #9923, #1600, #3771, #10508, #3081 ) ) ;
#636=EDGE_CURVE ( 'NONE', #381, #12883, #3392, .T. ) ;
#639=CIRCLE ( 'NONE', #8141, 0.7007874015748031260 ) ;
#641=CARTESIAN_POINT ( 'NONE',  ( -0.4854723491485721798, 1.043263280880422528, 0.3484785681409913738 ) ) ;
#644=CIRCLE ( 'NONE', #13900, 0.5590551181102362266 ) ;
#649=DIRECTION ( 'NONE',  ( 0.000000000000000000, 1.000000000000000000, 0.000000000000000000 ) ) ;
#654=AXIS2_PLACEMENT_3D ( 'NONE', #11086, #7331, #1541 ) ;
#655=VECTOR ( 'NONE', #5792, 39.37007874015748143 ) ;
#656=ORIENTED_EDGE ( 'NONE', *, *, #11224, .F. ) ;
#660=PLANE ( 'NONE',  #160 ) ;
#666=CIRCLE ( 'NONE', #1915, 0.03937007874015751446 ) ;
#667=DIRECTION ( 'NONE',  ( 0.5000000000000041078, -0.000000000000000000, 0.8660254037844363761 ) ) ;
#673=CIRCLE ( 'NONE', #9428, 0.5433070866141731514 ) ;
#676=ORIENTED_EDGE ( 'NONE', *, *, #10676, .F. ) ;
#677=VERTEX_POINT ( 'NONE', #1517 ) ;
#680=AXIS2_PLACEMENT_3D ( 'NONE', #10803, #14428, #249 ) ;
#689=DIRECTION ( 'NONE',  ( -0.000000000000000000, -1.000000000000000000, -0.000000000000000000 ) ) ;
#692=VERTEX_POINT ( 'NONE', #1587 ) ;
#693=EDGE_CURVE ( 'NONE', #3049, #677, #1886, .T. ) ;
#695=AXIS2_PLACEMENT_3D ( 'NONE', #14577, #5477, #1890 ) ;
#696=ORIENTED_EDGE ( 'NONE', *, *, #4848, .T. ) ;
#697=VERTEX_POINT ( 'NONE', #13496 ) ;
#698=TOROIDAL_SURFACE ( 'NONE', #4699, 0.7007874015748031260, 0.007874015748031495954 ) ;
#700=FACE_OUTER_BOUND ( 'NONE', #4412, .T. ) ;
#702=EDGE_CURVE ( 'NONE', #15270, #10400, #1155, .T. ) ;
#703=DIRECTION ( 'NONE',  ( 0.000000000000000000, 0.000000000000000000, 1.000000000000000000 ) ) ;
#704=CARTESIAN_POINT ( 'NONE',  ( 0.4478092776764652783, 1.043307086614173373, 0.3267337836880532809 ) ) ;
#715=VERTEX_POINT ( 'NONE', #6041 ) ;
#716=AXIS2_PLACEMENT_3D ( 'NONE', #1330, #14567, #13245 ) ;
#721=CARTESIAN_POINT ( 'NONE',  ( 0.000000000000000000, 0.000000000000000000, 0.000000000000000000 ) ) ;
#724=CARTESIAN_POINT ( 'NONE',  ( -0.4861941749621833675, 1.338582677165354395, 0.3488953144687877983 ) ) ;
#727=LINE ( 'NONE', #4011, #1925 ) ;
#728=CARTESIAN_POINT ( 'NONE',  ( -0.4861941749621833675, 1.338582677165354395, 0.3488953144687877983 ) ) ;
#730=CARTESIAN_POINT ( 'NONE',  ( 0.000000000000000000, 0.000000000000000000, -0.5905511811023621549 ) ) ;
#731=VERTEX_POINT ( 'NONE', #3864 ) ;
#751=ORIENTED_EDGE ( 'NONE', *, *, #6123, .T. ) ;
#752=EDGE_CURVE ( 'NONE', #6519, #4716, #5141, .T. ) ;
#758=CARTESIAN_POINT ( 'NONE',  ( 0.4841913566216283216, 1.043107366814280734, 0.3477389867607208473 ) ) ;
#759=FACE_BOUND ( 'NONE', #6247, .T. ) ;
#760=EDGE_LOOP ( 'NONE', ( #2647, #10099, #14539, #11090 ) ) ;
#761=ORIENTED_EDGE ( 'NONE', *, *, #10931, .F. ) ;
#764=DIRECTION ( 'NONE',  ( 0.000000000000000000, 0.000000000000000000, -1.000000000000000000 ) ) ;
#769=CARTESIAN_POINT ( 'NONE',  ( 0.000000000000000000, 1.035433070866142113, 0.000000000000000000 ) ) ;
#772=CARTESIAN_POINT ( 'NONE',  ( -0.7796283024904574477, 1.190944881889763884, 0.3819276336347811607 ) ) ;
#773=DIRECTION ( 'NONE',  ( 0.000000000000000000, 0.000000000000000000, -1.000000000000000000 ) ) ;
#776=VERTEX_POINT ( 'NONE', #10995 ) ;
#779=ORIENTED_EDGE ( 'NONE', *, *, #7891, .F. ) ;
#780=EDGE_CURVE ( 'NONE', #25, #15217, #5492, .T. ) ;
#782=ADVANCED_FACE ( 'NONE', ( #12408, #13806 ), #660, .T. ) ;
#783=CARTESIAN_POINT ( 'NONE',  ( 0.000000000000000000, 2.393700787401575436, 0.000000000000000000 ) ) ;
#784=DIRECTION ( 'NONE',  ( 0.000000000000000000, 0.000000000000000000, 1.000000000000000000 ) ) ;
#789=DIRECTION ( 'NONE',  ( 0.000000000000000000, 0.000000000000000000, -1.000000000000000000 ) ) ;
#796=VERTEX_POINT ( 'NONE', #12639 ) ;
#804=ADVANCED_FACE ( 'NONE', ( #11143, #1678 ), #3068, .F. ) ;
#812=ORIENTED_EDGE ( 'NONE', *, *, #2440, .T. ) ;
#815=ORIENTED_EDGE ( 'NONE', *, *, #7483, .T. ) ;
#819=CARTESIAN_POINT ( 'NONE',  ( 0.6864776960422569463, 1.190944881889763884, 0.4645290592786023298 ) ) ;
#827=ORIENTED_EDGE ( 'NONE', *, *, #13928, .T. ) ;
#828=CIRCLE ( 'NONE', #11072, 0.7007874015748031260 ) ;
#830=CIRCLE ( 'NONE', #2083, 0.5826771653543306728 ) ;
#831=ORIENTED_EDGE ( 'NONE', *, *, #6721, .F. ) ;
#836=DIRECTION ( 'NONE',  ( 0.000000000000000000, 0.000000000000000000, 1.000000000000000000 ) ) ;
#839=VECTOR ( 'NONE', #7017, 39.37007874015748143 ) ;
#851=VERTEX_POINT ( 'NONE', #13886 ) ;
#855=CIRCLE ( 'NONE', #11365, 0.5905511811023621549 ) ;
#856=VERTEX_POINT ( 'NONE', #430 ) ;
#862=DIRECTION ( 'NONE',  ( -0.000000000000000000, -1.000000000000000000, -0.000000000000000000 ) ) ;
#863=VECTOR ( 'NONE', #13257, 39.37007874015748143 ) ;
#864=DIRECTION ( 'NONE',  ( 0.000000000000000000, 1.000000000000000000, 0.000000000000000000 ) ) ;
#872=AXIS2_PLACEMENT_3D ( 'NONE', #13790, #7826, #4231 ) ;
#879=AXIS2_PLACEMENT_3D ( 'NONE', #11902, #67, #11817 ) ;
#881=CIRCLE ( 'NONE', #8384, 0.007874015748031449116 ) ;
#883=AXIS2_PLACEMENT_3D ( 'NONE', #6783, #8220, #5691 ) ;
#889=EDGE_LOOP ( 'NONE', ( #5300, #4624, #9223, #8545, #11790, #12162, #13483 ) ) ;
#893=CARTESIAN_POINT ( 'NONE',  ( 8.582170482213735190E-17, 0.3228346456692913757, -0.7007874015748031260 ) ) ;
#903=ORIENTED_EDGE ( 'NONE', *, *, #9642, .T. ) ;
#922=ORIENTED_EDGE ( 'NONE', *, *, #780, .T. ) ;
#926=VECTOR ( 'NONE', #8716, 39.37007874015748143 ) ;
#931=DIRECTION ( 'NONE',  ( 0.8660254037844361541, 0.000000000000000000, -0.5000000000000042188 ) ) ;
#936=AXIS2_PLACEMENT_3D ( 'NONE', #5152, #9872, #6548 ) ;
#938=ORIENTED_EDGE ( 'NONE', *, *, #13456, .F. ) ;
#950=EDGE_CURVE ( 'NONE', #450, #856, #14205, .T. ) ;
#956=VECTOR ( 'NONE', #4035, 39.37007874015748143 ) ;
#957=DIRECTION ( 'NONE',  ( 0.000000000000000000, 0.000000000000000000, 1.000000000000000000 ) ) ;
#966=ORIENTED_EDGE ( 'NONE', *, *, #12026, .F. ) ;
#970=LINE ( 'NONE', #8966, #14340 ) ;
#979=DIRECTION ( 'NONE',  ( 1.000000000000000000, 0.000000000000000000, 0.000000000000000000 ) ) ;
#980=DIRECTION ( 'NONE',  ( 0.000000000000000000, 0.000000000000000000, 1.000000000000000000 ) ) ;
#999=( BOUNDED_CURVE ( )  B_SPLINE_CURVE ( 3, ( #2540, #2769, #12110, #13214 ),
 .UNSPECIFIED., .F., .T. ) 
 B_SPLINE_CURVE_WITH_KNOTS ( ( 4, 4 ),
 ( 3.141592653589793116, 4.712388980384689674 ),
 .UNSPECIFIED. ) 
 CURVE ( )  GEOMETRIC_REPRESENTATION_ITEM ( )  RATIONAL_B_SPLINE_CURVE ( ( 1.000000000000000000, 0.8047378541243649375, 0.8047378541243649375, 1.000000000000000000 ) ) 
 REPRESENTATION_ITEM ( '' )  );
#1005=ORIENTED_EDGE ( 'NONE', *, *, #4307, .F. ) ;
#1013=CARTESIAN_POINT ( 'NONE',  ( -0.5403775459648845203, 1.343094183513034778, 0.2394881783597615499 ) ) ;
#1014=DIRECTION ( 'NONE',  ( 1.000000000000000000, 0.000000000000000000, -1.224646799147353207E-16 ) ) ;
#1016=ORIENTED_EDGE ( 'NONE', *, *, #2937, .T. ) ;
#1018=DIRECTION ( 'NONE',  ( -1.224646799147352961E-16, 0.000000000000000000, -1.000000000000000000 ) ) ;
#1021=ORIENTED_EDGE ( 'NONE', *, *, #276, .F. ) ;
#1024=FACE_OUTER_BOUND ( 'NONE', #5897, .T. ) ;
#1027=DIRECTION ( 'NONE',  ( -0.000000000000000000, -0.000000000000000000, -1.000000000000000000 ) ) ;
#1031=CARTESIAN_POINT ( 'NONE',  ( 0.5412478373021326616, 1.035433070866141891, 0.2362233606508025163 ) ) ;
#1032=CARTESIAN_POINT ( 'NONE',  ( -0.06604848736013263499, 0.000000000000000000, -0.5868460571724355423 ) ) ;
#1034=DIRECTION ( 'NONE',  ( 0.000000000000000000, 0.000000000000000000, -1.000000000000000000 ) ) ;
#1035=ORIENTED_EDGE ( 'NONE', *, *, #10958, .T. ) ;
#1040=ORIENTED_EDGE ( 'NONE', *, *, #9642, .F. ) ;
#1041=B_SPLINE_CURVE_WITH_KNOTS ( 'NONE', 3,
 ( #1316, #2555, #10867, #4984 ),
 .UNSPECIFIED., .F., .F.,
 ( 4, 4 ),
 ( 0.000000000000000000, 2.119993237936519055E-05 ),
 .UNSPECIFIED. ) ;
#1042=DIRECTION ( 'NONE',  ( 0.000000000000000000, 1.000000000000000000, 0.000000000000000000 ) ) ;
#1052=DIRECTION ( 'NONE',  ( 1.224646799147343593E-16, 0.000000000000000000, -1.000000000000000000 ) ) ;
#1057=ORIENTED_EDGE ( 'NONE', *, *, #10874, .T. ) ;
#1070=DIRECTION ( 'NONE',  ( 0.000000000000000000, 0.000000000000000000, -1.000000000000000000 ) ) ;
#1072=EDGE_LOOP ( 'NONE', ( #11242, #14038, #2085, #1813 ) ) ;
#1074=ORIENTED_EDGE ( 'NONE', *, *, #9322, .F. ) ;
#1082=VECTOR ( 'NONE', #8513, 39.37007874015748143 ) ;
#1086=DIRECTION ( 'NONE',  ( -0.000000000000000000, -1.000000000000000000, -0.000000000000000000 ) ) ;
#1098=AXIS2_PLACEMENT_3D ( 'NONE', #9093, #12777, #13874 ) ;
#1100=LINE ( 'NONE', #13950, #15396 ) ;
#1109=CARTESIAN_POINT ( 'NONE',  ( -0.4815353412745217998, 1.041793866378536437, 0.3474236500605538125 ) ) ;
#1113=VECTOR ( 'NONE', #2240, 39.37007874015748143 ) ;
#1115=VECTOR ( 'NONE', #15463, 39.37007874015748143 ) ;
#1121=CARTESIAN_POINT ( 'NONE',  ( -0.4854723491485722353, 1.190944881889763884, 0.3484785681409914293 ) ) ;
#1130=DIRECTION ( 'NONE',  ( -1.000000000000000000, 0.000000000000000000, 0.000000000000000000 ) ) ;
#1140=AXIS2_PLACEMENT_3D ( 'NONE', #5537, #11445, #11679 ) ;
#1144=CIRCLE ( 'NONE', #11897, 0.007874015748031516770 ) ;
#1155=CIRCLE ( 'NONE', #3137, 0.007874015748031516770 ) ;
#1157=FACE_OUTER_BOUND ( 'NONE', #5396, .T. ) ;
#1166=VERTEX_POINT ( 'NONE', #12290 ) ;
#1171=DIRECTION ( 'NONE',  ( 0.8660254037844431485, 0.000000000000000000, 0.4999999999999918954 ) ) ;
#1179=ORIENTED_EDGE ( 'NONE', *, *, #8976, .T. ) ;
#1180=VERTEX_POINT ( 'NONE', #1787 ) ;
#1188=EDGE_CURVE ( 'NONE', #6757, #2760, #6860, .T. ) ;
#1192=CARTESIAN_POINT ( 'NONE',  ( -0.6864776960422505070, 1.190944881889763884, 0.4645290592786119332 ) ) ;
#1197=DIRECTION ( 'NONE',  ( 0.8660254037844362651, 4.956352788505159323E-16, -0.5000000000000041078 ) ) ;
#1201=AXIS2_PLACEMENT_3D ( 'NONE', #12954, #2288, #9341 ) ;
#1203=DIRECTION ( 'NONE',  ( 0.000000000000000000, 1.000000000000000000, 0.000000000000000000 ) ) ;
#1205=DIRECTION ( 'NONE',  ( 0.000000000000000000, 0.000000000000000000, -1.000000000000000000 ) ) ;
#1211=DIRECTION ( 'NONE',  ( -1.000000000000000000, -4.565061778886334044E-16, 0.000000000000000000 ) ) ;
#1213=DIRECTION ( 'NONE',  ( 0.000000000000000000, 0.000000000000000000, 1.000000000000000000 ) ) ;
#1216=FACE_BOUND ( 'NONE', #3530, .T. ) ;
#1219=ORIENTED_EDGE ( 'NONE', *, *, #2551, .T. ) ;
#1220=ORIENTED_EDGE ( 'NONE', *, *, #14480, .F. ) ;
#1222=AXIS2_PLACEMENT_3D ( 'NONE', #4060, #6407, #9963 ) ;
#1225=CARTESIAN_POINT ( 'NONE',  ( -0.5445274672588088505, 1.043307086614173373, 0.2461921031270815907 ) ) ;
#1231=CARTESIAN_POINT ( 'NONE',  ( 0.000000000000000000, 2.637795275590551825, 0.03937007874015747977 ) ) ;
#1232=DIRECTION ( 'NONE',  ( 0.000000000000000000, 0.000000000000000000, 1.000000000000000000 ) ) ;
#1240=ORIENTED_EDGE ( 'NONE', *, *, #15271, .F. ) ;
#1243=CARTESIAN_POINT ( 'NONE',  ( -0.1181102362204724254, 2.448818897637795367, 0.03937007874015747977 ) ) ;
#1246=DIRECTION ( 'NONE',  ( 1.000000000000000000, 0.000000000000000000, -1.224646799147353207E-16 ) ) ;
#1250=DIRECTION ( 'NONE',  ( 0.000000000000000000, 1.000000000000000000, 0.000000000000000000 ) ) ;
#1251=LINE ( 'NONE', #6004, #13665 ) ;
#1252=ORIENTED_EDGE ( 'NONE', *, *, #1964, .F. ) ;
#1254=VERTEX_POINT ( 'NONE', #3910 ) ;
#1266=B_SPLINE_CURVE_WITH_KNOTS ( 'NONE', 3,
 ( #12133, #3899, #13522, #2644 ),
 .UNSPECIFIED., .F., .F.,
 ( 4, 4 ),
 ( 0.0002461255424396390835, 0.0003583013531701043780 ),
 .UNSPECIFIED. ) ;
#1269=PRODUCT_DEFINITION_CONTEXT ( 'detailed design', #7577, 'design' ) ;
#1274=DIRECTION ( 'NONE',  ( 0.000000000000000000, 0.000000000000000000, -1.000000000000000000 ) ) ;
#1278=CARTESIAN_POINT ( 'NONE',  ( -3.379785373986829049E-18, 1.043307086614173596, 1.951319995474476809E-18 ) ) ;
#1282=CARTESIAN_POINT ( 'NONE',  ( 0.000000000000000000, 1.346456692913385877, 0.000000000000000000 ) ) ;
#1285=ADVANCED_FACE ( 'NONE', ( #6953 ), #1946, .T. ) ;
#1288=ORIENTED_EDGE ( 'NONE', *, *, #11461, .T. ) ;
#1313=CYLINDRICAL_SURFACE ( 'NONE', #6115, 0.05905511811023625435 ) ;
#1315=CARTESIAN_POINT ( 'NONE',  ( 0.06012952712669447641, 1.340161268289288499, -0.5902914708161598467 ) ) ;
#1316=CARTESIAN_POINT ( 'NONE',  ( 0.4854723491485768982, 1.043263280880422528, 0.3484785681409844904 ) ) ;
#1318=ORIENTED_EDGE ( 'NONE', *, *, #13456, .T. ) ;
#1319=ORIENTED_EDGE ( 'NONE', *, *, #8741, .T. ) ;
#1320=LINE ( 'NONE', #7337, #8879 ) ;
#1326=DIRECTION ( 'NONE',  ( 0.000000000000000000, 0.000000000000000000, -1.000000000000000000 ) ) ;
#1330=CARTESIAN_POINT ( 'NONE',  ( 0.000000000000000000, 2.637795275590551825, -0.03937007874015747977 ) ) ;
#1332=ORIENTED_EDGE ( 'NONE', *, *, #9121, .T. ) ;
#1333=AXIS2_PLACEMENT_3D ( 'NONE', #4553, #3474, #8247 ) ;
#1337=DIRECTION ( 'NONE',  ( -0.000000000000000000, -1.000000000000000000, -0.000000000000000000 ) ) ;
#1339=DIRECTION ( 'NONE',  ( -0.000000000000000000, -1.000000000000000000, -0.000000000000000000 ) ) ;
#1343=CARTESIAN_POINT ( 'NONE',  ( 0.6864776960422569463, 1.190944881889763884, 0.4645290592786023298 ) ) ;
#1348=TOROIDAL_SURFACE ( 'NONE', #1848, 0.5984251968503937480, 0.007874015748031495954 ) ;
#1349=TOROIDAL_SURFACE ( 'NONE', #603, 0.6614173228346456046, 0.007874015748031495954 ) ;
#1355=ORIENTED_EDGE ( 'NONE', *, *, #11027, .T. ) ;
#1360=STYLED_ITEM('',(#15505),#4199);
#1362=CARTESIAN_POINT ( 'NONE',  ( 0.000000000000000000, 1.409448818897637956, 0.000000000000000000 ) ) ;
#1364=PRODUCT_DEFINITION_FORMATION_WITH_SPECIFIED_SOURCE ( 'ANY', '', #309, .NOT_KNOWN. ) ;
#1371=CARTESIAN_POINT ( 'NONE',  ( 0.000000000000000000, 1.425196850393700920, 0.000000000000000000 ) ) ;
#1378=ADVANCED_FACE ( 'NONE', ( #11423, #700 ), #5457, .F. ) ;
#1384=EDGE_LOOP ( 'NONE', ( #10062, #14363 ) ) ;
#1388=EDGE_CURVE ( 'NONE', #7994, #5246, #4279, .T. ) ;
#1389=DIRECTION ( 'NONE',  ( -1.000000000000000000, 0.000000000000000000, 0.000000000000000000 ) ) ;
#1398=FACE_OUTER_BOUND ( 'NONE', #3786, .T. ) ;
#1399=DIRECTION ( 'NONE',  ( 0.000000000000000000, 0.000000000000000000, -1.000000000000000000 ) ) ;
#1408=EDGE_CURVE ( 'NONE', #12754, #11565, #12138, .T. ) ;
#1411=CIRCLE ( 'NONE', #11413, 0.007874015748031482076 ) ;
#1421=CARTESIAN_POINT ( 'NONE',  ( 0.5412478373021326616, 1.035433070866141891, 0.2362233606508025163 ) ) ;
#1424=ORIENTED_EDGE ( 'NONE', *, *, #4740, .F. ) ;
#1425=ORIENTED_EDGE ( 'NONE', *, *, #7203, .F. ) ;
#1428=VERTEX_POINT ( 'NONE', #10228 ) ;
#1430=CARTESIAN_POINT ( 'NONE',  ( 0.000000000000000000, 1.346456692913385877, -0.5905511811023621549 ) ) ;
#1433=CARTESIAN_POINT ( 'NONE',  ( 6.653592845761209348E-17, 0.04724409448818898960, 0.5433070866141731514 ) ) ;
#1434=AXIS2_PLACEMENT_3D ( 'NONE', #3064, #13735, #12317 ) ;
#1436=VERTEX_POINT ( 'NONE', #5263 ) ;
#1444=EDGE_LOOP ( 'NONE', ( #205, #7671 ) ) ;
#1447=AXIS2_PLACEMENT_3D ( 'NONE', #15423, #4689, #5922 ) ;
#1449=CARTESIAN_POINT ( 'NONE',  ( 2.025006518275150778E-17, -1.707404996040164512E-17, -0.1653543307086614012 ) ) ;
#1452=FACE_OUTER_BOUND ( 'NONE', #13767, .T. ) ;
#1454=DIRECTION ( 'NONE',  ( 0.000000000000000000, 0.000000000000000000, -1.000000000000000000 ) ) ;
#1457=FACE_OUTER_BOUND ( 'NONE', #6315, .T. ) ;
#1463=ADVANCED_FACE ( 'NONE', ( #4105 ), #2857, .F. ) ;
#1464=ORIENTED_EDGE ( 'NONE', *, *, #9361, .T. ) ;
#1467=AXIS2_PLACEMENT_3D ( 'NONE', #1192, #9560, #12932 ) ;
#1469=PLANE ( 'NONE',  #4835 ) ;
#1475=DIRECTION ( 'NONE',  ( -0.000000000000000000, -1.000000000000000000, -0.000000000000000000 ) ) ;
#1477=CARTESIAN_POINT ( 'NONE',  ( 0.000000000000000000, 0.000000000000000000, 0.000000000000000000 ) ) ;
#1478=CARTESIAN_POINT ( 'NONE',  ( 0.000000000000000000, 0.000000000000000000, 0.000000000000000000 ) ) ;
#1481=EDGE_CURVE ( 'NONE', #6389, #7333, #6762, .T. ) ;
#1484=EDGE_CURVE ( 'NONE', #8826, #2247, #8802, .T. ) ;
#1485=EDGE_LOOP ( 'NONE', ( #11055, #3153, #3263, #14893 ) ) ;
#1491=CARTESIAN_POINT ( 'NONE',  ( 0.7455328141524921737, 1.190944881889763884, 0.3622425942646917418 ) ) ;
#1498=ORIENTED_EDGE ( 'NONE', *, *, #14031, .T. ) ;
#1506=EDGE_LOOP ( 'NONE', ( #1005, #8758, #607, #6822 ) ) ;
#1510=CYLINDRICAL_SURFACE ( 'NONE', #14643, 0.03937007874015761855 ) ;
#1511=LINE ( 'NONE', #9578, #12213 ) ;
#1513=EDGE_LOOP ( 'NONE', ( #4241, #2382, #3075, #751 ) ) ;
#1515=EDGE_LOOP ( 'NONE', ( #15107, #239, #15385, #13752 ) ) ;
#1517=CARTESIAN_POINT ( 'NONE',  ( -0.05905511811023625435, 2.637795275590551825, -0.03937007874015747977 ) ) ;
#1521=CARTESIAN_POINT ( 'NONE',  ( 0.000000000000000000, 0.000000000000000000, 0.000000000000000000 ) ) ;
#1522=FACE_OUTER_BOUND ( 'NONE', #4390, .T. ) ;
#1527=CARTESIAN_POINT ( 'NONE',  ( -0.7455328141524873997, 1.190944881889763884, 0.3622425942647021779 ) ) ;
#1535=CARTESIAN_POINT ( 'NONE',  ( 0.000000000000000000, 2.401574803149606918, 0.000000000000000000 ) ) ;
#1537=DIRECTION ( 'NONE',  ( 0.000000000000000000, -1.000000000000000000, 0.000000000000000000 ) ) ;
#1541=DIRECTION ( 'NONE',  ( 0.000000000000000000, 0.000000000000000000, -1.000000000000000000 ) ) ;
#1542=VERTEX_POINT ( 'NONE', #5734 ) ;
#1544=VERTEX_POINT ( 'NONE', #8191 ) ;
#1546=VERTEX_POINT ( 'NONE', #8020 ) ;
#1547=EDGE_LOOP ( 'NONE', ( #7478, #5200, #12563, #14223 ) ) ;
#1550=DIRECTION ( 'NONE',  ( 0.000000000000000000, 1.000000000000000000, 0.000000000000000000 ) ) ;
#1557=ORIENTED_EDGE ( 'NONE', *, *, #11175, .F. ) ;
#1558=DIRECTION ( 'NONE',  ( 0.000000000000000000, 0.000000000000000000, 1.000000000000000000 ) ) ;
#1561=ORIENTED_EDGE ( 'NONE', *, *, #10820, .T. ) ;
#1563=ORIENTED_EDGE ( 'NONE', *, *, #6456, .T. ) ;
#1564=ORIENTED_EDGE ( 'NONE', *, *, #702, .F. ) ;
#1565=FACE_OUTER_BOUND ( 'NONE', #10973, .T. ) ;
#1574=CIRCLE ( 'NONE', #6567, 0.007874015748031449116 ) ;
#1581=EDGE_CURVE ( 'NONE', #12382, #11226, #11954, .T. ) ;
#1584=ORIENTED_EDGE ( 'NONE', *, *, #11099, .T. ) ;
#1587=CARTESIAN_POINT ( 'NONE',  ( 0.7796283024904624437, 1.190944881889763884, 0.3819276336347702805 ) ) ;
#1588=CIRCLE ( 'NONE', #5578, 0.5905511811023621549 ) ;
#1589=VECTOR ( 'NONE', #8066, 39.37007874015748143 ) ;
#1590=DIRECTION ( 'NONE',  ( -0.000000000000000000, -1.000000000000000000, -0.000000000000000000 ) ) ;
#1591=DIRECTION ( 'NONE',  ( -1.000000000000000000, -0.000000000000000000, -0.000000000000000000 ) ) ;
#1595=DIRECTION ( 'NONE',  ( -0.000000000000000000, -1.000000000000000000, -0.000000000000000000 ) ) ;
#1598=DIRECTION ( 'NONE',  ( 0.000000000000000000, 0.000000000000000000, 1.000000000000000000 ) ) ;
#1599=VERTEX_POINT ( 'NONE', #14926 ) ;
#1600=ADVANCED_FACE ( 'NONE', ( #10445 ), #8436, .F. ) ;
#1602=CIRCLE ( 'NONE', #7591, 0.7086614173228346081 ) ;
#1614=AXIS2_PLACEMENT_3D ( 'NONE', #7716, #12504, #10148 ) ;
#1615=TOROIDAL_SURFACE ( 'NONE', #3622, 0.5590551181102362266, 0.007874015748031495954 ) ;
#1623=B_SPLINE_CURVE_WITH_KNOTS ( 'NONE', 3,
 ( #499, #1669, #12040, #14822 ),
 .UNSPECIFIED., .F., .F.,
 ( 4, 4 ),
 ( 0.000000000000000000, 2.119993237936282563E-05 ),
 .UNSPECIFIED. ) ;
#1633=ORIENTED_EDGE ( 'NONE', *, *, #53, .T. ) ;
#1634=ORIENTED_EDGE ( 'NONE', *, *, #4954, .T. ) ;
#1642=CIRCLE ( 'NONE', #8139, 0.6692913385826770867 ) ;
#1644=AXIS2_PLACEMENT_3D ( 'NONE', #497, #14819, #5241 ) ;
#1647=DIRECTION ( 'NONE',  ( 0.000000000000000000, 0.000000000000000000, -1.000000000000000000 ) ) ;
#1649=CIRCLE ( 'NONE', #163, 0.5511811023622046335 ) ;
#1658=CIRCLE ( 'NONE', #11418, 0.007874015748031449116 ) ;
#1660=DIRECTION ( 'NONE',  ( 0.000000000000000000, 0.000000000000000000, 1.000000000000000000 ) ) ;
#1668=AXIS2_PLACEMENT_3D ( 'NONE', #1527, #4899, #3961 ) ;
#1669=CARTESIAN_POINT ( 'NONE',  ( -0.5447670804912987386, 1.043292445042268257, 0.2463304438913610228 ) ) ;
#1671=CIRCLE ( 'NONE', #186, 0.5905511811023621549 ) ;
#1672=VERTEX_POINT ( 'NONE', #10219 ) ;
#1678=FACE_OUTER_BOUND ( 'NONE', #11676, .T. ) ;
#1679=AXIS2_PLACEMENT_3D ( 'NONE', #9203, #13264, #2523 ) ;
#1695=VERTEX_POINT ( 'NONE', #6585 ) ;
#1696=DIRECTION ( 'NONE',  ( 0.4999999999999918954, -0.000000000000000000, -0.8660254037844431485 ) ) ;
#1699=AXIS2_PLACEMENT_3D ( 'NONE', #819, #5744, #4339 ) ;
#1703=CARTESIAN_POINT ( 'NONE',  ( 0.000000000000000000, 0.5984251968503937480, 0.000000000000000000 ) ) ;
#1705=PLANE ( 'NONE',  #2645 ) ;
#1708=DIRECTION ( 'NONE',  ( 0.000000000000000000, 0.000000000000000000, 1.000000000000000000 ) ) ;
#1709=DIRECTION ( 'NONE',  ( -0.000000000000000000, -1.000000000000000000, -0.000000000000000000 ) ) ;
#1712=VECTOR ( 'NONE', #2678, 39.37007874015748143 ) ;
#1715=ORIENTED_EDGE ( 'NONE', *, *, #14031, .F. ) ;
#1723=DIRECTION ( 'NONE',  ( -0.000000000000000000, -1.000000000000000000, -0.000000000000000000 ) ) ;
#1725=CIRCLE ( 'NONE', #9979, 0.05905511811023625435 ) ;
#1729=DIRECTION ( 'NONE',  ( 0.000000000000000000, 0.000000000000000000, 1.000000000000000000 ) ) ;
#1734=DIRECTION ( 'NONE',  ( 1.000000000000000000, -0.000000000000000000, 1.224646799147353207E-16 ) ) ;
#1735=CARTESIAN_POINT ( 'NONE',  ( 0.000000000000000000, 1.425196850393700920, -0.6614173228346456046 ) ) ;
#1736=CARTESIAN_POINT ( 'NONE',  ( 0.000000000000000000, 0.5511811023622046335, 0.000000000000000000 ) ) ;
#1737=DIRECTION ( 'NONE',  ( 2.309263891220325920E-14, 0.000000000000000000, -1.000000000000000000 ) ) ;
#1742=CARTESIAN_POINT ( 'NONE',  ( 0.05905511811023622659, 1.043307086614173373, -0.5511811023622047445 ) ) ;
#1747=ORIENTED_EDGE ( 'NONE', *, *, #5493, .T. ) ;
#1758=ADVANCED_FACE ( 'NONE', ( #5497 ), #13889, .F. ) ;
#1765=ORIENTED_EDGE ( 'NONE', *, *, #13389, .F. ) ;
#1766=ORIENTED_EDGE ( 'NONE', *, *, #11796, .T. ) ;
#1775=FACE_OUTER_BOUND ( 'NONE', #1513, .T. ) ;
#1779=ORIENTED_EDGE ( 'NONE', *, *, #1964, .T. ) ;
#1785=EDGE_CURVE ( 'NONE', #6404, #9753, #8402, .T. ) ;
#1787=CARTESIAN_POINT ( 'NONE',  ( -0.05905511811023622659, 1.338582677165354395, -0.8267716535433070613 ) ) ;
#1790=CARTESIAN_POINT ( 'NONE',  ( 0.000000000000000000, 1.614173228346457156, 0.5590551181102362266 ) ) ;
#1793=CARTESIAN_POINT ( 'NONE',  ( 0.05905511811023622659, 1.043263280880422528, -0.5946706712680680518 ) ) ;
#1796=CARTESIAN_POINT ( 'NONE',  ( 8.196454954923229282E-17, 0.3622047244094487306, 0.6692913385826770867 ) ) ;
#1800=EDGE_CURVE ( 'NONE', #14240, #8264, #12703, .T. ) ;
#1806=LINE ( 'NONE', #3933, #926 ) ;
#1812=ORIENTED_EDGE ( 'NONE', *, *, #5688, .F. ) ;
#1813=ORIENTED_EDGE ( 'NONE', *, *, #5250, .F. ) ;
#1826=AXIS2_PLACEMENT_3D ( 'NONE', #1491, #2499, #6239 ) ;
#1832=VERTEX_POINT ( 'NONE', #30 ) ;
#1836=TOROIDAL_SURFACE ( 'NONE', #10600, 0.5826771653543306728, 0.007874015748031495954 ) ;
#1841=LINE ( 'NONE', #1928, #8964 ) ;
#1844=DIRECTION ( 'NONE',  ( 0.000000000000000000, 0.000000000000000000, 1.000000000000000000 ) ) ;
#1848=AXIS2_PLACEMENT_3D ( 'NONE', #490, #13408, #411 ) ;
#1849=CARTESIAN_POINT ( 'NONE',  ( 8.678599364036360127E-17, 0.000000000000000000, 0.7086614173228346081 ) ) ;
#1855=ORIENTED_EDGE ( 'NONE', *, *, #12657, .T. ) ;
#1859=CARTESIAN_POINT ( 'NONE',  ( -0.5412478373021294420, 1.346456692913385877, 0.2362233606508100381 ) ) ;
#1863=CARTESIAN_POINT ( 'NONE',  ( 0.000000000000000000, 2.637795275590551825, 0.03937007874015747977 ) ) ;
#1875=CIRCLE ( 'NONE', #8892, 0.03937007874015761161 ) ;
#1880=CIRCLE ( 'NONE', #3130, 0.007874015748031516770 ) ;
#1886=CIRCLE ( 'NONE', #3887, 0.05905511811023625435 ) ;
#1887=DIRECTION ( 'NONE',  ( -0.000000000000000000, -1.000000000000000000, -0.000000000000000000 ) ) ;
#1890=DIRECTION ( 'NONE',  ( 0.000000000000000000, 0.000000000000000000, -1.000000000000000000 ) ) ;
#1894=ORIENTED_EDGE ( 'NONE', *, *, #10527, .F. ) ;
#1898=CYLINDRICAL_SURFACE ( 'NONE', #8851, 0.007874015748031516770 ) ;
#1902=TOROIDAL_SURFACE ( 'NONE', #2145, 0.5590551181102362266, 0.007874015748031495954 ) ;
#1907=AXIS2_PLACEMENT_3D ( 'NONE', #12265, #5984, #6048 ) ;
#1915=AXIS2_PLACEMENT_3D ( 'NONE', #11004, #7251, #443 ) ;
#1922=VERTEX_POINT ( 'NONE', #8711 ) ;
#1923=ORIENTED_EDGE ( 'NONE', *, *, #950, .T. ) ;
#1924=ORIENTED_EDGE ( 'NONE', *, *, #13619, .F. ) ;
#1925=VECTOR ( 'NONE', #7524, 39.37007874015748854 ) ;
#1928=CARTESIAN_POINT ( 'NONE',  ( 0.1181102362204724116, 2.448818897637795367, 0.03937007874015747977 ) ) ;
#1932=FACE_OUTER_BOUND ( 'NONE', #10268, .T. ) ;
#1934=CARTESIAN_POINT ( 'NONE',  ( 0.4854723491485768982, 1.043263280880422528, 0.3484785681409844904 ) ) ;
#1946=CYLINDRICAL_SURFACE ( 'NONE', #2115, 0.1476377952755905942 ) ;
#1949=DIRECTION ( 'NONE',  ( -1.224646799147343593E-16, 0.000000000000000000, -1.000000000000000000 ) ) ;
#1951=CARTESIAN_POINT ( 'NONE',  ( 0.000000000000000000, 0.007874015748031480341, 0.000000000000000000 ) ) ;
#1955=ADVANCED_FACE ( 'NONE', ( #6188 ), #10980, .F. ) ;
#1957=CARTESIAN_POINT ( 'NONE',  ( 0.000000000000000000, 0.5984251968503937480, 0.000000000000000000 ) ) ;
#1958=AXIS2_PLACEMENT_3D ( 'NONE', #13009, #15443, #84 ) ;
#1964=EDGE_CURVE ( 'NONE', #6858, #12158, #10700, .T. ) ;
#1965=ORIENTED_EDGE ( 'NONE', *, *, #116, .T. ) ;
#1969=CARTESIAN_POINT ( 'NONE',  ( 0.000000000000000000, 1.338582677165354395, -0.5984251968503937480 ) ) ;
#1975=DIRECTION ( 'NONE',  ( 1.000000000000000000, -0.000000000000000000, 1.224646799147353207E-16 ) ) ;
#1976=CARTESIAN_POINT ( 'NONE',  ( -0.4787089944775287931, 1.040121464703355647, 0.3474236500605662470 ) ) ;
#1985=DIRECTION ( 'NONE',  ( 0.8660254037844362651, 0.000000000000000000, -0.5000000000000041078 ) ) ;
#1992=DIRECTION ( 'NONE',  ( 0.000000000000000000, 0.000000000000000000, 1.000000000000000000 ) ) ;
#1994=DIRECTION ( 'NONE',  ( 0.000000000000000000, 0.000000000000000000, 1.000000000000000000 ) ) ;
#1995=ORIENTED_EDGE ( 'NONE', *, *, #12608, .F. ) ;
#2003=FACE_OUTER_BOUND ( 'NONE', #7442, .T. ) ;
#2006=ORIENTED_EDGE ( 'NONE', *, *, #6413, .F. ) ;
#2008=EDGE_LOOP ( 'NONE', ( #12285, #8123, #9758, #5973, #12336, #12520 ) ) ;
#2012=EDGE_CURVE ( 'NONE', #8683, #13359, #3194, .T. ) ;
#2013=DIRECTION ( 'NONE',  ( -0.000000000000000000, 1.000000000000000000, -0.000000000000000000 ) ) ;
#2029=FACE_OUTER_BOUND ( 'NONE', #14239, .T. ) ;
#2031=FACE_BOUND ( 'NONE', #5280, .T. ) ;
#2032=CARTESIAN_POINT ( 'NONE',  ( -0.4861941749621833675, 1.043307086614173373, 0.3488953144687877983 ) ) ;
#2035=EDGE_CURVE ( 'NONE', #2747, #2525, #10658, .T. ) ;
#2036=DIRECTION ( 'NONE',  ( -4.292327424963333000E-16, -1.000000000000000000, -2.478176394252540219E-16 ) ) ;
#2042=ORIENTED_EDGE ( 'NONE', *, *, #11662, .F. ) ;
#2043=ORIENTED_EDGE ( 'NONE', *, *, #5220, .F. ) ;
#2052=ORIENTED_EDGE ( 'NONE', *, *, #3042, .F. ) ;
#2057=DIRECTION ( 'NONE',  ( 0.000000000000000000, -1.000000000000000000, -0.000000000000000000 ) ) ;
#2071=CYLINDRICAL_SURFACE ( 'NONE', #10401, 0.1181102362204724532 ) ;
#2076=CIRCLE ( 'NONE', #4078, 0.1574803149606299191 ) ;
#2078=EDGE_CURVE ( 'NONE', #2233, #7918, #6989, .T. ) ;
#2083=AXIS2_PLACEMENT_3D ( 'NONE', #15033, #1723, #481 ) ;
#2085=ORIENTED_EDGE ( 'NONE', *, *, #260, .T. ) ;
#2086=DIRECTION ( 'NONE',  ( 1.000000000000000000, -0.000000000000000000, 1.224646799147353207E-16 ) ) ;
#2092=AXIS2_PLACEMENT_3D ( 'NONE', #14384, #11220, #7175 ) ;
#2103=AXIS2_PLACEMENT_3D ( 'NONE', #1371, #11967, #9766 ) ;
#2104=CIRCLE ( 'NONE', #11611, 0.6614173228346456046 ) ;
#2107=VERTEX_POINT ( 'NONE', #5062 ) ;
#2109=DIRECTION ( 'NONE',  ( 0.000000000000000000, 1.000000000000000000, 0.000000000000000000 ) ) ;
#2111=DIRECTION ( 'NONE',  ( 0.000000000000000000, 0.000000000000000000, -1.000000000000000000 ) ) ;
#2115=AXIS2_PLACEMENT_3D ( 'NONE', #11498, #9153, #931 ) ;
#2116=TOROIDAL_SURFACE ( 'NONE', #9875, 0.5590551181102362266, 0.007874015748031495954 ) ;
#2125=CARTESIAN_POINT ( 'NONE',  ( -0.1259842519685039353, 2.448818897637795367, 0.000000000000000000 ) ) ;
#2130=CIRCLE ( 'NONE', #5619, 0.007874015748031449116 ) ;
#2143=CARTESIAN_POINT ( 'NONE',  ( -0.05905511811023622659, 1.190944881889763884, -0.8267716535433072833 ) ) ;
#2145=AXIS2_PLACEMENT_3D ( 'NONE', #4825, #5837, #12995 ) ;
#2149=ADVANCED_FACE ( 'NONE', ( #6084, #12231 ), #173, .T. ) ;
#2150=VERTEX_POINT ( 'NONE', #3686 ) ;
#2154=CARTESIAN_POINT ( 'NONE',  ( 0.6864776960422569463, 1.190944881889763884, 0.4645290592786023298 ) ) ;
#2157=EDGE_CURVE ( 'NONE', #5195, #14360, #6573, .T. ) ;
#2158=EDGE_LOOP ( 'NONE', ( #11810, #6074, #5323, #11592 ) ) ;
#2163=DIRECTION ( 'NONE',  ( -8.673617379884029309E-17, 1.000000000000000000, 0.000000000000000000 ) ) ;
#2175=VECTOR ( 'NONE', #10335, 39.37007874015748143 ) ;
#2179=CARTESIAN_POINT ( 'NONE',  ( 0.000000000000000000, 1.409448818897637956, 0.000000000000000000 ) ) ;
#2187=VERTEX_POINT ( 'NONE', #3992 ) ;
#2189=FACE_OUTER_BOUND ( 'NONE', #2298, .T. ) ;
#2194=CIRCLE ( 'NONE', #8440, 0.5905511811023621549 ) ;
#2195=VERTEX_POINT ( 'NONE', #8766 ) ;
#2206=LINE ( 'NONE', #13172, #7597 ) ;
#2208=CARTESIAN_POINT ( 'NONE',  ( -0.05905511811023622659, 1.338582677165354395, -0.5952259495879738127 ) ) ;
#2209=DIRECTION ( 'NONE',  ( -0.000000000000000000, -1.000000000000000000, -0.000000000000000000 ) ) ;
#2210=VERTEX_POINT ( 'NONE', #7343 ) ;
#2227=EDGE_CURVE ( 'NONE', #14454, #562, #14343, .T. ) ;
#2229=ORIENTED_EDGE ( 'NONE', *, *, #447, .F. ) ;
#2233=VERTEX_POINT ( 'NONE', #13708 ) ;
#2240=DIRECTION ( 'NONE',  ( -0.000000000000000000, -1.000000000000000000, -0.000000000000000000 ) ) ;
#2247=VERTEX_POINT ( 'NONE', #2797 ) ;
#2249=ORIENTED_EDGE ( 'NONE', *, *, #15271, .T. ) ;
#2251=EDGE_CURVE ( 'NONE', #10793, #11857, #830, .T. ) ;
#2253=CARTESIAN_POINT ( 'NONE',  ( -0.5424655050177918936, 1.338877451511696570, 0.2450016286721715675 ) ) ;
#2254=DIRECTION ( 'NONE',  ( 0.000000000000000000, -1.000000000000000000, -0.000000000000000000 ) ) ;
#2272=CARTESIAN_POINT ( 'NONE',  ( 7.232166136696967594E-17, 2.433070866141732846, 0.5905511811023621549 ) ) ;
#2277=ORIENTED_EDGE ( 'NONE', *, *, #2035, .T. ) ;
#2278=EDGE_CURVE ( 'NONE', #10886, #1546, #4139, .T. ) ;
#2280=ORIENTED_EDGE ( 'NONE', *, *, #7586, .T. ) ;
#2283=CARTESIAN_POINT ( 'NONE',  ( 0.000000000000000000, 1.338582677165354395, 0.000000000000000000 ) ) ;
#2285=DIRECTION ( 'NONE',  ( 0.000000000000000000, 0.000000000000000000, 1.000000000000000000 ) ) ;
#2288=DIRECTION ( 'NONE',  ( -0.000000000000000000, -1.000000000000000000, -0.000000000000000000 ) ) ;
#2291=DIRECTION ( 'NONE',  ( -0.000000000000000000, -1.000000000000000000, -0.000000000000000000 ) ) ;
#2297=ORIENTED_EDGE ( 'NONE', *, *, #15172, .T. ) ;
#2298=EDGE_LOOP ( 'NONE', ( #2229, #3388, #1634, #14662 ) ) ;
#2308=ORIENTED_EDGE ( 'NONE', *, *, #4857, .T. ) ;
#2313=EDGE_CURVE ( 'NONE', #4716, #7918, #14093, .T. ) ;
#2320=ORIENTED_EDGE ( 'NONE', *, *, #4446, .F. ) ;
#2330=ORIENTED_EDGE ( 'NONE', *, *, #11953, .F. ) ;
#2336=CIRCLE ( 'NONE', #8853, 0.5905511811023621549 ) ;
#2340=DIRECTION ( 'NONE',  ( 0.000000000000000000, 0.000000000000000000, 1.000000000000000000 ) ) ;
#2344=CARTESIAN_POINT ( 'NONE',  ( -0.06438893898759806556, 1.344775570699244582, -0.5870328364109891339 ) ) ;
#2346=CARTESIAN_POINT ( 'NONE',  ( 0.5405798186813290940, 1.344775570699301648, 0.2377539613195566448 ) ) ;
#2348=ORIENTED_EDGE ( 'NONE', *, *, #13177, .F. ) ;
#2350=CIRCLE ( 'NONE', #13608, 0.007874015748031516770 ) ;
#2356=DIRECTION ( 'NONE',  ( 0.000000000000000000, 0.000000000000000000, -1.000000000000000000 ) ) ;
#2357=AXIS2_PLACEMENT_3D ( 'NONE', #9664, #1339, #1274 ) ;
#2361=CARTESIAN_POINT ( 'NONE',  ( -0.05905511811023622659, 1.043307086614173373, -0.5955041639236610118 ) ) ;
#2368=DIRECTION ( 'NONE',  ( 1.000000000000000000, 0.000000000000000000, 0.000000000000000000 ) ) ;
#2369=EDGE_CURVE ( 'NONE', #6293, #13266, #15343, .T. ) ;
#2382=ORIENTED_EDGE ( 'NONE', *, *, #10303, .T. ) ;
#2389=CIRCLE ( 'NONE', #395, 0.007874015748031482076 ) ;
#2391=CARTESIAN_POINT ( 'NONE',  ( 0.4815353412745612127, 0.000000000000000000, 0.3552976658085785222 ) ) ;
#2395=FACE_OUTER_BOUND ( 'NONE', #9903, .T. ) ;
#2398=VECTOR ( 'NONE', #689, 39.37007874015748143 ) ;
#2399=ORIENTED_EDGE ( 'NONE', *, *, #13951, .T. ) ;
#2400=AXIS2_PLACEMENT_3D ( 'NONE', #14720, #13375, #9711 ) ;
#2405=B_SPLINE_CURVE_WITH_KNOTS ( 'NONE', 3,
 ( #180, #2346, #4939, #4780, #7131, #14338 ),
 .UNSPECIFIED., .F., .F.,
 ( 4, 2, 4 ),
 ( -2.828444569872989946E-06, 0.0001777364543001158713, 0.0003583013531701047033 ),
 .UNSPECIFIED. ) ;
#2407=DIRECTION ( 'NONE',  ( -1.000000000000000000, -0.000000000000000000, -0.000000000000000000 ) ) ;
#2410=DIRECTION ( 'NONE',  ( 0.000000000000000000, -1.000000000000000000, 0.000000000000000000 ) ) ;
#2417=CARTESIAN_POINT ( 'NONE',  ( 0.000000000000000000, 0.5433070866141731514, 0.6614173228346456046 ) ) ;
#2422=VERTEX_POINT ( 'NONE', #4894 ) ;
#2427=CARTESIAN_POINT ( 'NONE',  ( -0.1181102362204724254, 2.448818897637795367, -0.03937007874015747977 ) ) ;
#2428=CARTESIAN_POINT ( 'NONE',  ( -0.5412721729274213578, 1.041728495490239492, 0.2430720373988195515 ) ) ;
#2432=EDGE_CURVE ( 'NONE', #851, #15395, #8427, .T. ) ;
#2440=EDGE_CURVE ( 'NONE', #11092, #10823, #13580, .T. ) ;
#2443=AXIS2_PLACEMENT_3D ( 'NONE', #12707, #12475, #6729 ) ;
#2462=ORIENTED_EDGE ( 'NONE', *, *, #8039, .F. ) ;
#2477=CARTESIAN_POINT ( 'NONE',  ( 0.05905511811023622659, 1.043307086614173373, -0.5511811023622047445 ) ) ;
#2489=DIRECTION ( 'NONE',  ( 0.000000000000000000, 0.000000000000000000, 1.000000000000000000 ) ) ;
#2496=ADVANCED_FACE ( 'NONE', ( #1457 ), #9607, .T. ) ;
#2498=DIRECTION ( 'NONE',  ( 0.000000000000000000, 0.000000000000000000, 1.000000000000000000 ) ) ;
#2499=DIRECTION ( 'NONE',  ( 0.4999999999999920064, 0.000000000000000000, -0.8660254037844433705 ) ) ;
#2500=DIRECTION ( 'NONE',  ( 0.000000000000000000, 1.000000000000000000, 0.000000000000000000 ) ) ;
#2505=ORIENTED_EDGE ( 'NONE', *, *, #513, .T. ) ;
#2514=CARTESIAN_POINT ( 'NONE',  ( -0.06604848736013260724, 1.035433070866141891, -0.5868460571724354313 ) ) ;
#2521=CARTESIAN_POINT ( 'NONE',  ( 0.000000000000000000, 0.3464566929133857109, 0.000000000000000000 ) ) ;
#2523=DIRECTION ( 'NONE',  ( 0.000000000000000000, 0.000000000000000000, -1.000000000000000000 ) ) ;
#2525=VERTEX_POINT ( 'NONE', #7710 ) ;
#2527=ADVANCED_FACE ( 'NONE', ( #6512 ), #15101, .F. ) ;
#2540=CARTESIAN_POINT ( 'NONE',  ( 0.1181102362204724254, 2.448818897637795367, 0.03937007874015747977 ) ) ;
#2541=ORIENTED_EDGE ( 'NONE', *, *, #8873, .T. ) ;
#2542=ORIENTED_EDGE ( 'NONE', *, *, #151, .F. ) ;
#2543=VERTEX_POINT ( 'NONE', #3167 ) ;
#2544=LINE ( 'NONE', #12045, #8352 ) ;
#2548=CARTESIAN_POINT ( 'NONE',  ( 0.000000000000000000, 0.03937007874015749365, -0.1653543307086614012 ) ) ;
#2551=EDGE_CURVE ( 'NONE', #11565, #8556, #3091, .T. ) ;
#2555=CARTESIAN_POINT ( 'NONE',  ( 0.4857119623810668974, 1.043292445042268257, 0.3486169089052639780 ) ) ;
#2556=ORIENTED_EDGE ( 'NONE', *, *, #4159, .F. ) ;
#2558=ORIENTED_EDGE ( 'NONE', *, *, #11812, .T. ) ;
#2562=CIRCLE ( 'NONE', #5302, 0.007874015748031449116 ) ;
#2563=VECTOR ( 'NONE', #14637, 39.37007874015748143 ) ;
#2587=AXIS2_PLACEMENT_3D ( 'NONE', #15225, #8078, #11470 ) ;
#2595=DIRECTION ( 'NONE',  ( -0.000000000000000000, -1.000000000000000000, -0.000000000000000000 ) ) ;
#2608=DIRECTION ( 'NONE',  ( -1.000000000000000000, 0.000000000000000000, 0.000000000000000000 ) ) ;
#2612=DIRECTION ( 'NONE',  ( 0.000000000000000000, 0.000000000000000000, 1.000000000000000000 ) ) ;
#2618=CARTESIAN_POINT ( 'NONE',  ( 0.000000000000000000, 1.661417322834646049, 0.000000000000000000 ) ) ;
#2625=DIRECTION ( 'NONE',  ( 0.000000000000000000, 1.000000000000000000, 0.000000000000000000 ) ) ;
#2626=CARTESIAN_POINT ( 'NONE',  ( 0.05905511811023622659, 1.190944881889763884, -0.8267716535433072833 ) ) ;
#2633=TOROIDAL_SURFACE ( 'NONE', #2888, 0.5590551181102362266, 0.007874015748031495954 ) ;
#2634=AXIS2_PLACEMENT_3D ( 'NONE', #3594, #14415, #9489 ) ;
#2643=CARTESIAN_POINT ( 'NONE',  ( 0.06278630405416070481, 1.343094588453027427, -0.5877245205702892328 ) ) ;
#2644=CARTESIAN_POINT ( 'NONE',  ( 0.4854723491485768982, 1.338626482899105241, 0.3484785681409844904 ) ) ;
#2645=AXIS2_PLACEMENT_3D ( 'NONE', #7414, #1537, #10069 ) ;
#2646=ORIENTED_EDGE ( 'NONE', *, *, #9551, .F. ) ;
#2647=ORIENTED_EDGE ( 'NONE', *, *, #3095, .T. ) ;
#2649=EDGE_LOOP ( 'NONE', ( #8900, #14490, #13904, #14741 ) ) ;
#2663=ORIENTED_EDGE ( 'NONE', *, *, #13739, .T. ) ;
#2674=CARTESIAN_POINT ( 'NONE',  ( 0.000000000000000000, 0.3543307086614172485, -0.5590551181102362266 ) ) ;
#2678=DIRECTION ( 'NONE',  ( -1.000000000000000000, -0.000000000000000000, -0.000000000000000000 ) ) ;
#2682=PLANE ( 'NONE',  #10423 ) ;
#2694=AXIS2_PLACEMENT_3D ( 'NONE', #4301, #7600, #7922 ) ;
#2700=DIRECTION ( 'NONE',  ( 0.000000000000000000, 0.000000000000000000, -1.000000000000000000 ) ) ;
#2701=DIRECTION ( 'NONE',  ( 1.224646799147353947E-16, 0.000000000000000000, -1.000000000000000000 ) ) ;
#2710=ORIENTED_EDGE ( 'NONE', *, *, #13432, .T. ) ;
#2716=LINE ( 'NONE', #14543, #228 ) ;
#2721=LINE ( 'NONE', #9778, #1082 ) ;
#2724=CARTESIAN_POINT ( 'NONE',  ( 0.05905511811023621271, 1.338877467290996659, -0.5922895726594219479 ) ) ;
#2725=CYLINDRICAL_SURFACE ( 'NONE', #407, 0.03937007874015761161 ) ;
#2730=EDGE_LOOP ( 'NONE', ( #12534, #3767, #11892, #9821 ) ) ;
#2736=CARTESIAN_POINT ( 'NONE',  ( -0.5412478373021294420, 1.035433070866141891, 0.2362233606508100381 ) ) ;
#2737=DIRECTION ( 'NONE',  ( 0.000000000000000000, 0.000000000000000000, 1.000000000000000000 ) ) ;
#2738=CARTESIAN_POINT ( 'NONE',  ( 0.05905511811023622659, 1.043263280880422528, -0.5946706712680680518 ) ) ;
#2747=VERTEX_POINT ( 'NONE', #3060 ) ;
#2750=DIRECTION ( 'NONE',  ( 0.000000000000000000, 0.000000000000000000, 1.000000000000000000 ) ) ;
#2756=EDGE_CURVE ( 'NONE', #3058, #9379, #2336, .T. ) ;
#2760=VERTEX_POINT ( 'NONE', #11454 ) ;
#2761=EDGE_LOOP ( 'NONE', ( #3278, #5053, #7756, #12785 ) ) ;
#2763=CARTESIAN_POINT ( 'NONE',  ( 0.000000000000000000, 2.637795275590551825, -0.03937007874015747977 ) ) ;
#2767=CARTESIAN_POINT ( 'NONE',  ( 0.000000000000000000, 1.614173228346457156, 0.000000000000000000 ) ) ;
#2768=CARTESIAN_POINT ( 'NONE',  ( 7.232166136696967594E-17, 0.3070866141732283561, 0.5905511811023621549 ) ) ;
#2769=CARTESIAN_POINT ( 'NONE',  ( 0.1181102362204723977, 2.444206406002937815, 0.03937007874015747977 ) ) ;
#2771=ORIENTED_EDGE ( 'NONE', *, *, #2313, .T. ) ;
#2774=EDGE_CURVE ( 'NONE', #11438, #6858, #15369, .T. ) ;
#2779=DIRECTION ( 'NONE',  ( -4.292327424963298981E-16, 1.000000000000000000, 2.478176394252600369E-16 ) ) ;
#2780=DIRECTION ( 'NONE',  ( -0.000000000000000000, -1.000000000000000000, -0.000000000000000000 ) ) ;
#2785=ADVANCED_FACE ( 'NONE', ( #6803, #7759 ), #558, .F. ) ;
#2788=ORIENTED_EDGE ( 'NONE', *, *, #3042, .T. ) ;
#2789=ORIENTED_EDGE ( 'NONE', *, *, #8631, .F. ) ;
#2790=ADVANCED_FACE ( 'NONE', ( #7996 ), #1349, .F. ) ;
#2792=DIRECTION ( 'NONE',  ( 0.000000000000000000, 0.000000000000000000, -1.000000000000000000 ) ) ;
#2795=DIRECTION ( 'NONE',  ( 0.000000000000000000, 0.000000000000000000, 1.000000000000000000 ) ) ;
#2797=CARTESIAN_POINT ( 'NONE',  ( 0.7205731843802273273, 1.190944881889763884, 0.4842140986486808130 ) ) ;
#2801=CYLINDRICAL_SURFACE ( 'NONE', #11695, 0.5511811023622046335 ) ;
#2804=DIRECTION ( 'NONE',  ( 0.000000000000000000, 0.000000000000000000, 1.000000000000000000 ) ) ;
#2806=ORIENTED_EDGE ( 'NONE', *, *, #6170, .T. ) ;
#2808=ADVANCED_FACE ( 'NONE', ( #15049 ), #13099, .T. ) ;
#2809=EDGE_CURVE ( 'NONE', #12857, #5735, #5399, .T. ) ;
#2814=CARTESIAN_POINT ( 'NONE',  ( 0.1181102362204724254, 2.448818897637795367, -0.03937007874015747977 ) ) ;
#2816=ORIENTED_EDGE ( 'NONE', *, *, #2227, .F. ) ;
#2818=CARTESIAN_POINT ( 'NONE',  ( 0.000000000000000000, 0.3622047244094487306, 0.000000000000000000 ) ) ;
#2826=ADVANCED_FACE ( 'NONE', ( #7690 ), #1836, .T. ) ;
#2828=ORIENTED_EDGE ( 'NONE', *, *, #36, .T. ) ;
#2829=CARTESIAN_POINT ( 'NONE',  ( 0.000000000000000000, 1.425196850393700920, 0.000000000000000000 ) ) ;
#2835=EDGE_CURVE ( 'NONE', #11283, #6857, #12601, .T. ) ;
#2837=CARTESIAN_POINT ( 'NONE',  ( 0.05905511811023622659, 1.190944881889763884, -0.8267716535433072833 ) ) ;
#2842=DIRECTION ( 'NONE',  ( -1.000000000000000000, -0.000000000000000000, -0.000000000000000000 ) ) ;
#2846=ORIENTED_EDGE ( 'NONE', *, *, #9322, .T. ) ;
#2847=AXIS2_PLACEMENT_3D ( 'NONE', #1521, #14606, #1454 ) ;
#2849=AXIS2_PLACEMENT_3D ( 'NONE', #14886, #13713, #13940 ) ;
#2852=EDGE_LOOP ( 'NONE', ( #7750, #8181, #91, #8167 ) ) ;
#2854=DIRECTION ( 'NONE',  ( 0.000000000000000000, 0.000000000000000000, 1.000000000000000000 ) ) ;
#2857=TOROIDAL_SURFACE ( 'NONE', #1614, 0.5433070866141731514, 0.007874015748031495954 ) ;
#2861=DIRECTION ( 'NONE',  ( 1.000000000000000000, 0.000000000000000000, 0.000000000000000000 ) ) ;
#2864=CARTESIAN_POINT ( 'NONE',  ( 0.000000000000000000, -1.707404996040164512E-17, 0.000000000000000000 ) ) ;
#2866=DIRECTION ( 'NONE',  ( -1.000000000000000000, 0.000000000000000000, 0.000000000000000000 ) ) ;
#2874=EDGE_LOOP ( 'NONE', ( #10650, #237, #8309, #5642 ) ) ;
#2878=EDGE_CURVE ( 'NONE', #3695, #14360, #2350, .T. ) ;
#2881=ADVANCED_FACE ( 'NONE', ( #6498 ), #11285, .F. ) ;
#2884=DIRECTION ( 'NONE',  ( 0.000000000000000000, 0.000000000000000000, -1.000000000000000000 ) ) ;
#2887=DIRECTION ( 'NONE',  ( -0.000000000000000000, -1.000000000000000000, -0.000000000000000000 ) ) ;
#2888=AXIS2_PLACEMENT_3D ( 'NONE', #2521, #6113, #7296 ) ;
#2895=DIRECTION ( 'NONE',  ( -0.000000000000000000, -1.000000000000000000, -0.000000000000000000 ) ) ;
#2896=AXIS2_PLACEMENT_3D ( 'NONE', #2391, #8029, #8204 ) ;
#2897=CARTESIAN_POINT ( 'NONE',  ( 0.000000000000000000, 2.637795275590551825, 0.03937007874015747977 ) ) ;
#2898=VERTEX_POINT ( 'NONE', #10504 ) ;
#2904=EDGE_CURVE ( 'NONE', #1832, #10243, #2206, .T. ) ;
#2906=EDGE_CURVE ( 'NONE', #6855, #5486, #7461, .T. ) ;
#2912=ORIENTED_EDGE ( 'NONE', *, *, #10564, .F. ) ;
#2915=CARTESIAN_POINT ( 'NONE',  ( -0.4857119623810620679, 1.338597318737259734, 0.3486169089052708614 ) ) ;
#2916=DIRECTION ( 'NONE',  ( -0.000000000000000000, -1.000000000000000000, -0.000000000000000000 ) ) ;
#2924=ORIENTED_EDGE ( 'NONE', *, *, #5467, .F. ) ;
#2926=CARTESIAN_POINT ( 'NONE',  ( 0.5452492930724234244, 1.043307086614173373, 0.2466088494548703824 ) ) ;
#2927=DIRECTION ( 'NONE',  ( 0.000000000000000000, -1.000000000000000000, -0.000000000000000000 ) ) ;
#2935=LINE ( 'NONE', #5255, #380 ) ;
#2937=EDGE_CURVE ( 'NONE', #6855, #13421, #6980, .T. ) ;
#2939=VECTOR ( 'NONE', #1027, 39.37007874015748143 ) ;
#2941=CARTESIAN_POINT ( 'NONE',  ( 0.000000000000000000, 2.393700787401575436, 0.000000000000000000 ) ) ;
#2959=ORIENTED_EDGE ( 'NONE', *, *, #13432, .F. ) ;
#2970=DIRECTION ( 'NONE',  ( 0.000000000000000000, 0.000000000000000000, 1.000000000000000000 ) ) ;
#2972=CARTESIAN_POINT ( 'NONE',  ( 6.653592845761209348E-17, 2.393700787401575436, -0.5433070866141731514 ) ) ;
#2973=DIRECTION ( 'NONE',  ( -0.000000000000000000, -1.000000000000000000, -0.000000000000000000 ) ) ;
#2974=DIRECTION ( 'NONE',  ( -1.000000000000000000, -0.000000000000000000, -0.000000000000000000 ) ) ;
#2978=CARTESIAN_POINT ( 'NONE',  ( -0.5452492930724200937, 1.338582677165354395, 0.2466088494548780152 ) ) ;
#2980=ORIENTED_EDGE ( 'NONE', *, *, #3489, .F. ) ;
#2982=ORIENTED_EDGE ( 'NONE', *, *, #11548, .T. ) ;
#2983=CARTESIAN_POINT ( 'NONE',  ( 0.05905511811023622659, 1.043307086614173373, -0.5946706712680680518 ) ) ;
#2989=FACE_OUTER_BOUND ( 'NONE', #14058, .T. ) ;
#2998=ORIENTED_EDGE ( 'NONE', *, *, #14986, .F. ) ;
#3002=DIRECTION ( 'NONE',  ( -0.000000000000000000, 1.000000000000000000, -0.000000000000000000 ) ) ;
#3012=CARTESIAN_POINT ( 'NONE',  ( 0.4854723491485768982, 1.338626482899105241, 0.3484785681409844904 ) ) ;
#3014=ADVANCED_FACE ( 'NONE', ( #3532 ), #3294, .F. ) ;
#3021=CARTESIAN_POINT ( 'NONE',  ( 0.000000000000000000, 0.3464566929133857109, 0.000000000000000000 ) ) ;
#3024=ADVANCED_FACE ( 'NONE', ( #6312, #7437 ), #14429, .F. ) ;
#3042=EDGE_CURVE ( 'NONE', #13421, #8067, #855, .T. ) ;
#3043=LINE ( 'NONE', #704, #14660 ) ;
#3047=ORIENTED_EDGE ( 'NONE', *, *, #11140, .T. ) ;
#3049=VERTEX_POINT ( 'NONE', #5153 ) ;
#3050=EDGE_LOOP ( 'NONE', ( #4973, #14863, #1563, #9783 ) ) ;
#3054=CARTESIAN_POINT ( 'NONE',  ( 0.000000000000000000, 0.000000000000000000, 0.000000000000000000 ) ) ;
#3058=VERTEX_POINT ( 'NONE', #1421 ) ;
#3059=DIRECTION ( 'NONE',  ( -0.000000000000000000, -1.000000000000000000, -0.000000000000000000 ) ) ;
#3060=CARTESIAN_POINT ( 'NONE',  ( -0.1181102362204724532, 2.637795275590551825, 0.03937007874015747977 ) ) ;
#3063=ORIENTED_EDGE ( 'NONE', *, *, #12522, .T. ) ;
#3064=CARTESIAN_POINT ( 'NONE',  ( 0.000000000000000000, 1.338582677165354395, 0.000000000000000000 ) ) ;
#3067=DIRECTION ( 'NONE',  ( -1.000000000000000000, 0.000000000000000000, 0.000000000000000000 ) ) ;
#3068=PLANE ( 'NONE',  #14667 ) ;
#3074=CARTESIAN_POINT ( 'NONE',  ( 0.5452492930724234244, 1.338582677165354395, 0.2466088494548705212 ) ) ;
#3075=ORIENTED_EDGE ( 'NONE', *, *, #11980, .T. ) ;
#3076=CARTESIAN_POINT ( 'NONE',  ( 0.000000000000000000, 0.5826771653543306728, 0.000000000000000000 ) ) ;
#3079=AXIS2_PLACEMENT_3D ( 'NONE', #8502, #11969, #1232 ) ;
#3081=ADVANCED_FACE ( 'NONE', ( #12691 ), #10858, .T. ) ;
#3083=DIRECTION ( 'NONE',  ( 0.000000000000000000, 0.000000000000000000, 1.000000000000000000 ) ) ;
#3086=AXIS2_PLACEMENT_3D ( 'NONE', #5008, #9805, #536 ) ;
#3087=EDGE_LOOP ( 'NONE', ( #1035, #8598, #3983, #300 ) ) ;
#3089=ORIENTED_EDGE ( 'NONE', *, *, #5220, .T. ) ;
#3091=CIRCLE ( 'NONE', #13849, 0.6614173228346456046 ) ;
#3093=PLANE ( 'NONE',  #9616 ) ;
#3095=EDGE_CURVE ( 'NONE', #12818, #15326, #8617, .T. ) ;
#3102=AXIS2_PLACEMENT_3D ( 'NONE', #11499, #6865, #9003 ) ;
#3107=ADVANCED_FACE ( 'NONE', ( #11577 ), #4609, .F. ) ;
#3112=ORIENTED_EDGE ( 'NONE', *, *, #2035, .F. ) ;
#3114=AXIS2_PLACEMENT_3D ( 'NONE', #12038, #13350, #14535 ) ;
#3115=CIRCLE ( 'NONE', #13873, 0.5511811023622046335 ) ;
#3126=EDGE_CURVE ( 'NONE', #10243, #2898, #9355, .T. ) ;
#3130=AXIS2_PLACEMENT_3D ( 'NONE', #8857, #1734, #13726 ) ;
#3134=CARTESIAN_POINT ( 'NONE',  ( -0.6692913385826770867, 0.5511811023622046335, 0.000000000000000000 ) ) ;
#3136=AXIS2_PLACEMENT_3D ( 'NONE', #2818, #2916, #9975 ) ;
#3137=AXIS2_PLACEMENT_3D ( 'NONE', #7532, #6267, #208 ) ;
#3145=CARTESIAN_POINT ( 'NONE',  ( 0.000000000000000000, 0.5433070866141731514, 0.000000000000000000 ) ) ;
#3153=ORIENTED_EDGE ( 'NONE', *, *, #5609, .F. ) ;
#3159=CARTESIAN_POINT ( 'NONE',  ( -0.5511811023622046335, 1.417322834645669438, 0.000000000000000000 ) ) ;
#3163=AXIS2_PLACEMENT_3D ( 'NONE', #8803, #4184, #3083 ) ;
#3165=VERTEX_POINT ( 'NONE', #1796 ) ;
#3167=CARTESIAN_POINT ( 'NONE',  ( 0.1259842519685039353, 2.440944881889763884, 0.04724409448818898266 ) ) ;
#3170=CARTESIAN_POINT ( 'NONE',  ( 0.4859532342797860394, 1.338582677165354395, 0.3487562073009374264 ) ) ;
#3172=EDGE_LOOP ( 'NONE', ( #4781, #1747, #6330, #11606 ) ) ;
#3176=EDGE_CURVE ( 'NONE', #13376, #14592, #13785, .T. ) ;
#3178=AXIS2_PLACEMENT_3D ( 'NONE', #416, #11284, #7595 ) ;
#3183=CARTESIAN_POINT ( 'NONE',  ( 8.582170482213735190E-17, 1.385826771653543510, -0.7007874015748031260 ) ) ;
#3184=( BOUNDED_CURVE ( )  B_SPLINE_CURVE ( 3, ( #8377, #3453, #11922, #2427 ),
 .UNSPECIFIED., .F., .T. ) 
 B_SPLINE_CURVE_WITH_KNOTS ( ( 4, 4 ),
 ( 4.712388980384689674, 6.283185307179586232 ),
 .UNSPECIFIED. ) 
 CURVE ( )  GEOMETRIC_REPRESENTATION_ITEM ( )  RATIONAL_B_SPLINE_CURVE ( ( 1.000000000000000000, 0.8047378541243649375, 0.8047378541243649375, 1.000000000000000000 ) ) 
 REPRESENTATION_ITEM ( '' )  );
#3190=CIRCLE ( 'NONE', #13204, 0.1653543307086614012 ) ;
#3192=ORIENTED_EDGE ( 'NONE', *, *, #3960, .F. ) ;
#3194=CIRCLE ( 'NONE', #2443, 0.007874015748031516770 ) ;
#3206=DIRECTION ( 'NONE',  ( -0.000000000000000000, -1.000000000000000000, 4.956352788505160310E-16 ) ) ;
#3210=DIRECTION ( 'NONE',  ( -1.224646799147353700E-16, 0.000000000000000000, -1.000000000000000000 ) ) ;
#3212=ORIENTED_EDGE ( 'NONE', *, *, #15142, .F. ) ;
#3214=AXIS2_PLACEMENT_3D ( 'NONE', #13541, #5230, #2804 ) ;
#3215=ADVANCED_FACE ( 'NONE', ( #2189 ), #13112, .T. ) ;
#3217=B_SPLINE_CURVE_WITH_KNOTS ( 'NONE', 3,
 ( #10880, #14495, #2428, #9558, #9643, #2736 ),
 .UNSPECIFIED., .F., .F.,
 ( 4, 2, 4 ),
 ( 0.000000000000000000, 0.0001791382075655885420, 0.0003582764151311770839 ),
 .UNSPECIFIED. ) ;
#3218=FACE_OUTER_BOUND ( 'NONE', #8324, .T. ) ;
#3223=FACE_OUTER_BOUND ( 'NONE', #13130, .T. ) ;
#3228=CARTESIAN_POINT ( 'NONE',  ( -0.7086614173228346081, 1.653543307086614567, 0.000000000000000000 ) ) ;
#3235=EDGE_CURVE ( 'NONE', #2210, #7634, #3850, .T. ) ;
#3247=CARTESIAN_POINT ( 'NONE',  ( -0.7086614173228346081, 0.5905511811023621549, 0.000000000000000000 ) ) ;
#3249=ORIENTED_EDGE ( 'NONE', *, *, #14299, .F. ) ;
#3251=CARTESIAN_POINT ( 'NONE',  ( 0.5452492930724234244, 1.043307086614173373, 0.2466088494548703824 ) ) ;
#3252=ORIENTED_EDGE ( 'NONE', *, *, #15255, .F. ) ;
#3257=CARTESIAN_POINT ( 'NONE',  ( 6.750021727583836750E-17, 0.5590551181102362266, 0.5511811023622046335 ) ) ;
#3258=FACE_OUTER_BOUND ( 'NONE', #6830, .T. ) ;
#3261=CARTESIAN_POINT ( 'NONE',  ( 0.5484644751328278112, 0.000000000000000000, 0.2393730054594799261 ) ) ;
#3263=ORIENTED_EDGE ( 'NONE', *, *, #8404, .T. ) ;
#3264=EDGE_LOOP ( 'NONE', ( #1021, #4368, #6682, #3063 ) ) ;
#3272=CARTESIAN_POINT ( 'NONE',  ( 0.000000000000000000, 0.3149606299212598381, 0.7007874015748031260 ) ) ;
#3276=CARTESIAN_POINT ( 'NONE',  ( 0.4861941749621881415, 1.043307086614173373, 0.3488953144687809704 ) ) ;
#3277=CARTESIAN_POINT ( 'NONE',  ( 0.000000000000000000, 0.3149606299212598381, 0.5984251968503937480 ) ) ;
#3278=ORIENTED_EDGE ( 'NONE', *, *, #4424, .T. ) ;
#3279=B_SPLINE_CURVE_WITH_KNOTS ( 'NONE', 3,
 ( #10224, #3170, #8895, #3012 ),
 .UNSPECIFIED., .F., .F.,
 ( 4, 4 ),
 ( 0.000000000000000000, 2.119993237936537351E-05 ),
 .UNSPECIFIED. ) ;
#3283=CARTESIAN_POINT ( 'NONE',  ( -0.5511811023622046335, 2.401574803149606918, 0.000000000000000000 ) ) ;
#3294=CYLINDRICAL_SURFACE ( 'NONE', #8865, 0.05905511811023625435 ) ;
#3296=LINE ( 'NONE', #730, #1589 ) ;
#3299=CARTESIAN_POINT ( 'NONE',  ( 0.4861941749621881415, 1.338582677165354395, 0.3488953144687809704 ) ) ;
#3309=DIRECTION ( 'NONE',  ( 0.000000000000000000, 0.000000000000000000, 1.000000000000000000 ) ) ;
#3312=CARTESIAN_POINT ( 'NONE',  ( -0.1259842519685039353, 2.440944881889763884, 0.04724409448818898266 ) ) ;
#3314=EDGE_CURVE ( 'NONE', #2187, #6409, #9780, .T. ) ;
#3317=CARTESIAN_POINT ( 'NONE',  ( 0.5447670804913020692, 1.043292445042268257, 0.2463304438913534455 ) ) ;
#3320=ADVANCED_FACE ( 'NONE', ( #1398 ), #3746, .T. ) ;
#3323=AXIS2_PLACEMENT_3D ( 'NONE', #1951, #6713, #11504 ) ;
#3326=FACE_OUTER_BOUND ( 'NONE', #2874, .T. ) ;
#3327=LINE ( 'NONE', #8269, #5630 ) ;
#3338=ORIENTED_EDGE ( 'NONE', *, *, #10463, .F. ) ;
#3342=CIRCLE ( 'NONE', #9859, 0.6692913385826770867 ) ;
#3349=DIRECTION ( 'NONE',  ( 0.000000000000000000, 1.000000000000000000, 0.000000000000000000 ) ) ;
#3351=ORIENTED_EDGE ( 'NONE', *, *, #5580, .T. ) ;
#3359=AXIS2_PLACEMENT_3D ( 'NONE', #14184, #13163, #170 ) ;
#3360=AXIS2_PLACEMENT_3D ( 'NONE', #13398, #179, #7278 ) ;
#3361=ORIENTED_EDGE ( 'NONE', *, *, #3691, .T. ) ;
#3363=EDGE_CURVE ( 'NONE', #6293, #381, #9332, .T. ) ;
#3388=ORIENTED_EDGE ( 'NONE', *, *, #3429, .F. ) ;
#3392=CIRCLE ( 'NONE', #5369, 0.007874015748031516770 ) ;
#3396=EDGE_CURVE ( 'NONE', #14687, #12371, #6323, .T. ) ;
#3401=ORIENTED_EDGE ( 'NONE', *, *, #8404, .F. ) ;
#3405=AXIS2_PLACEMENT_3D ( 'NONE', #9310, #1086, #2489 ) ;
#3406=DIRECTION ( 'NONE',  ( 1.224646799147353947E-16, 0.000000000000000000, -1.000000000000000000 ) ) ;
#3413=EDGE_CURVE ( 'NONE', #6757, #3049, #13521, .T. ) ;
#3419=B_SPLINE_CURVE_WITH_KNOTS ( 'NONE', 3,
 ( #12706, #5476, #10264, #641 ),
 .UNSPECIFIED., .F., .F.,
 ( 4, 4 ),
 ( 0.000000000000000000, 2.119993237936282563E-05 ),
 .UNSPECIFIED. ) ;
#3429=EDGE_CURVE ( 'NONE', #3736, #12889, #828, .T. ) ;
#3436=AXIS2_PLACEMENT_3D ( 'NONE', #9023, #13794, #6565 ) ;
#3441=CARTESIAN_POINT ( 'NONE',  ( -0.5412723129863770133, 1.340161119985692428, 0.2430722610364171865 ) ) ;
#3453=CARTESIAN_POINT ( 'NONE',  ( -0.1213717603336464113, 2.440944881889763884, -0.04263160285333146560 ) ) ;
#3454=DIRECTION ( 'NONE',  ( -0.000000000000000000, -1.000000000000000000, -0.000000000000000000 ) ) ;
#3471=DIMENSIONAL_EXPONENTS ( 1.000000000000000000, 0.000000000000000000, 0.000000000000000000, 0.000000000000000000, 0.000000000000000000, 0.000000000000000000, 0.000000000000000000 ) ;
#3474=DIRECTION ( 'NONE',  ( -0.000000000000000000, -1.000000000000000000, -0.000000000000000000 ) ) ;
#3485=DIRECTION ( 'NONE',  ( 0.4999999999999919509, -0.000000000000000000, -0.8660254037844432595 ) ) ;
#3486=ADVANCED_FACE ( 'NONE', ( #1775, #7795 ), #6698, .F. ) ;
#3488=EDGE_LOOP ( 'NONE', ( #13506, #7460, #8521, #13032 ) ) ;
#3489=EDGE_CURVE ( 'NONE', #4456, #11475, #4122, .T. ) ;
#3492=ORIENTED_EDGE ( 'NONE', *, *, #1785, .F. ) ;
#3494=CARTESIAN_POINT ( 'NONE',  ( 0.000000000000000000, 1.377952755905512028, 0.000000000000000000 ) ) ;
#3502=FACE_OUTER_BOUND ( 'NONE', #9550, .T. ) ;
#3504=ORIENTED_EDGE ( 'NONE', *, *, #11371, .T. ) ;
#3505=EDGE_CURVE ( 'NONE', #8683, #288, #12587, .T. ) ;
#3507=EDGE_LOOP ( 'NONE', ( #13396, #3903, #2998, #10477, #5703 ) ) ;
#3510=APPLICATION_CONTEXT ( 'automotive_design' ) ;
#3516=ORIENTED_EDGE ( 'NONE', *, *, #6456, .F. ) ;
#3519=ORIENTED_EDGE ( 'NONE', *, *, #14792, .T. ) ;
#3520=EDGE_LOOP ( 'NONE', ( #10805, #9206, #76, #9471 ) ) ;
#3527=CARTESIAN_POINT ( 'NONE',  ( 0.000000000000000000, 0.5590551181102362266, 0.5590551181102362266 ) ) ;
#3530=EDGE_LOOP ( 'NONE', ( #2806, #12968 ) ) ;
#3532=FACE_OUTER_BOUND ( 'NONE', #10549, .T. ) ;
#3547=DIRECTION ( 'NONE',  ( 1.000000000000000000, -0.000000000000000000, 1.224646799147353207E-16 ) ) ;
#3549=ORIENTED_EDGE ( 'NONE', *, *, #12608, .T. ) ;
#3553=ADVANCED_FACE ( 'NONE', ( #7554 ), #8833, .F. ) ;
#3567=ORIENTED_EDGE ( 'NONE', *, *, #9619, .T. ) ;
#3568=ORIENTED_EDGE ( 'NONE', *, *, #9306, .T. ) ;
#3571=EDGE_CURVE ( 'NONE', #856, #14746, #8771, .T. ) ;
#3572=FACE_BOUND ( 'NONE', #6977, .T. ) ;
#3579=TOROIDAL_SURFACE ( 'NONE', #10086, 0.5984251968503937480, 0.007874015748031495954 ) ;
#3581=FACE_OUTER_BOUND ( 'NONE', #4290, .T. ) ;
#3585=DIRECTION ( 'NONE',  ( 1.000000000000000000, 0.000000000000000000, -1.224646799147353207E-16 ) ) ;
#3594=CARTESIAN_POINT ( 'NONE',  ( -0.1574803149606299191, -1.743072535964414816E-17, 0.000000000000000000 ) ) ;
#3599=CARTESIAN_POINT ( 'NONE',  ( 0.4478092776764652783, 1.043307086614173373, 0.3267337836880532809 ) ) ;
#3601=DIRECTION ( 'NONE',  ( 1.000000000000000000, 0.000000000000000000, -1.224646799147353207E-16 ) ) ;
#3602=ADVANCED_FACE ( 'NONE', ( #3502 ), #8575, .F. ) ;
#3603=DIRECTION ( 'NONE',  ( -1.000000000000000000, 0.000000000000000000, 0.000000000000000000 ) ) ;
#3608=CIRCLE ( 'NONE', #6832, 0.007874015748031516770 ) ;
#3615=AXIS2_PLACEMENT_3D ( 'NONE', #6816, #9436, #15226 ) ;
#3619=LINE ( 'NONE', #1121, #14597 ) ;
#3622=AXIS2_PLACEMENT_3D ( 'NONE', #3873, #4808, #14698 ) ;
#3623=CIRCLE ( 'NONE', #3359, 0.1476377952755905942 ) ;
#3624=CARTESIAN_POINT ( 'NONE',  ( 6.750021727583836750E-17, 0.000000000000000000, 0.5511811023622046335 ) ) ;
#3631=CARTESIAN_POINT ( 'NONE',  ( 0.05905511811023622659, 1.190944881889763884, -0.8267716535433072833 ) ) ;
#3647=VECTOR ( 'NONE', #957, 39.37007874015748143 ) ;
#3650=DIRECTION ( 'NONE',  ( 0.4999999999999918954, -0.000000000000000000, -0.8660254037844431485 ) ) ;
#3660=ORIENTED_EDGE ( 'NONE', *, *, #11856, .T. ) ;
#3665=CIRCLE ( 'NONE', #13167, 0.007874015748031449116 ) ;
#3671=TOROIDAL_SURFACE ( 'NONE', #13921, 0.5433070866141731514, 0.007874015748031495954 ) ;
#3672=CARTESIAN_POINT ( 'NONE',  ( 0.000000000000000000, 0.000000000000000000, -0.7086614173228346081 ) ) ;
#3683=VECTOR ( 'NONE', #15105, 39.37007874015747433 ) ;
#3686=CARTESIAN_POINT ( 'NONE',  ( 6.701807286672523049E-17, 0.03937007874015749365, 0.5433070866141731514 ) ) ;
#3687=CARTESIAN_POINT ( 'NONE',  ( 0.000000000000000000, 2.448818897637795367, 0.04724409448818898266 ) ) ;
#3691=EDGE_CURVE ( 'NONE', #7200, #1542, #6851, .T. ) ;
#3695=VERTEX_POINT ( 'NONE', #11560 ) ;
#3701=FACE_OUTER_BOUND ( 'NONE', #6675, .T. ) ;
#3707=CARTESIAN_POINT ( 'NONE',  ( 0.000000000000000000, 0.007874015748031480341, 0.000000000000000000 ) ) ;
#3716=ORIENTED_EDGE ( 'NONE', *, *, #6055, .F. ) ;
#3719=AXIS2_PLACEMENT_3D ( 'NONE', #3890, #8671, #3806 ) ;
#3728=DIRECTION ( 'NONE',  ( -0.000000000000000000, -1.000000000000000000, -0.000000000000000000 ) ) ;
#3736=VERTEX_POINT ( 'NONE', #9600 ) ;
#3740=FACE_OUTER_BOUND ( 'NONE', #14665, .T. ) ;
#3743=CARTESIAN_POINT ( 'NONE',  ( 8.196454954923229282E-17, 1.425196850393700920, 0.6692913385826770867 ) ) ;
#3746=CYLINDRICAL_SURFACE ( 'NONE', #13833, 0.5905511811023621549 ) ;
#3755=EDGE_CURVE ( 'NONE', #562, #14454, #9347, .T. ) ;
#3765=PLANE ( 'NONE',  #716 ) ;
#3766=ORIENTED_EDGE ( 'NONE', *, *, #11912, .T. ) ;
#3767=ORIENTED_EDGE ( 'NONE', *, *, #3489, .T. ) ;
#3771=ADVANCED_FACE ( 'NONE', ( #2395 ), #6318, .T. ) ;
#3772=CARTESIAN_POINT ( 'NONE',  ( 8.196454954923229282E-17, 0.000000000000000000, 0.6692913385826770867 ) ) ;
#3776=LINE ( 'NONE', #2814, #12723 ) ;
#3778=EDGE_LOOP ( 'NONE', ( #10435, #11353, #831, #1252 ) ) ;
#3786=EDGE_LOOP ( 'NONE', ( #13035, #2505, #11045, #2556 ) ) ;
#3787=ORIENTED_EDGE ( 'NONE', *, *, #5519, .F. ) ;
#3788=ORIENTED_EDGE ( 'NONE', *, *, #2278, .T. ) ;
#3789=DIRECTION ( 'NONE',  ( 0.000000000000000000, 0.000000000000000000, -1.000000000000000000 ) ) ;
#3791=DIRECTION ( 'NONE',  ( 0.000000000000000000, 1.000000000000000000, 0.000000000000000000 ) ) ;
#3799=DIRECTION ( 'NONE',  ( 0.000000000000000000, 0.000000000000000000, -1.000000000000000000 ) ) ;
#3800=DIRECTION ( 'NONE',  ( -0.000000000000000000, -1.000000000000000000, -0.000000000000000000 ) ) ;
#3802=EDGE_CURVE ( 'NONE', #12827, #796, #1623, .T. ) ;
#3803=ORIENTED_EDGE ( 'NONE', *, *, #3413, .F. ) ;
#3804=ORIENTED_EDGE ( 'NONE', *, *, #8820, .T. ) ;
#3806=DIRECTION ( 'NONE',  ( 0.000000000000000000, 0.000000000000000000, -1.000000000000000000 ) ) ;
#3813=CARTESIAN_POINT ( 'NONE',  ( 0.000000000000000000, 1.385826771653543510, 0.000000000000000000 ) ) ;
#3815=ORIENTED_EDGE ( 'NONE', *, *, #8873, .F. ) ;
#3817=ORIENTED_EDGE ( 'NONE', *, *, #14916, .T. ) ;
#3822=VECTOR ( 'NONE', #9532, 39.37007874015748143 ) ;
#3824=CARTESIAN_POINT ( 'NONE',  ( -0.4815353412745217998, 1.340095897400991110, 0.3474236500605538125 ) ) ;
#3834=AXIS2_PLACEMENT_3D ( 'NONE', #11060, #346, #9910 ) ;
#3841=CARTESIAN_POINT ( 'NONE',  ( 8.630384923125046426E-17, 0.5905511811023621549, 0.7007874015748031260 ) ) ;
#3848=CIRCLE ( 'NONE', #10354, 0.5905511811023621549 ) ;
#3850=CIRCLE ( 'NONE', #12615, 0.007874015748031516770 ) ;
#3854=EDGE_LOOP ( 'NONE', ( #1220, #1766, #922, #11113 ) ) ;
#3856=AXIS2_PLACEMENT_3D ( 'NONE', #11426, #6711, #703 ) ;
#3862=AXIS2_PLACEMENT_3D ( 'NONE', #5311, #7129, #1197 ) ;
#3864=CARTESIAN_POINT ( 'NONE',  ( 8.148240514011916814E-17, 1.417322834645669438, 0.6614173228346456046 ) ) ;
#3873=CARTESIAN_POINT ( 'NONE',  ( 0.000000000000000000, 1.409448818897637956, 0.000000000000000000 ) ) ;
#3875=AXIS2_PLACEMENT_3D ( 'NONE', #11300, #2842, #13571 ) ;
#3887=AXIS2_PLACEMENT_3D ( 'NONE', #2763, #14458, #6124 ) ;
#3888=DIRECTION ( 'NONE',  ( -0.000000000000000000, -1.000000000000000000, -0.000000000000000000 ) ) ;
#3890=CARTESIAN_POINT ( 'NONE',  ( 0.000000000000000000, 0.000000000000000000, 0.000000000000000000 ) ) ;
#3894=DIRECTION ( 'NONE',  ( 1.000000000000000000, 0.000000000000000000, -0.000000000000000000 ) ) ;
#3896=DIRECTION ( 'NONE',  ( -0.000000000000000000, -1.000000000000000000, -0.000000000000000000 ) ) ;
#3898=DIRECTION ( 'NONE',  ( -0.000000000000000000, -1.000000000000000000, -0.000000000000000000 ) ) ;
#3899=CARTESIAN_POINT ( 'NONE',  ( 0.4828087445803717070, 1.339342401112375125, 0.3474236500605413780 ) ) ;
#3900=AXIS2_PLACEMENT_3D ( 'NONE', #10004, #3896, #8676 ) ;
#3903=ORIENTED_EDGE ( 'NONE', *, *, #9121, .F. ) ;
#3907=ORIENTED_EDGE ( 'NONE', *, *, #12859, .T. ) ;
#3909=DIRECTION ( 'NONE',  ( 0.000000000000000000, 0.000000000000000000, -1.000000000000000000 ) ) ;
#3910=CARTESIAN_POINT ( 'NONE',  ( 0.000000000000000000, 0.3464566929133857109, -0.5511811023622046335 ) ) ;
#3911=CIRCLE ( 'NONE', #5406, 0.5433070866141731514 ) ;
#3915=CARTESIAN_POINT ( 'NONE',  ( -0.4787092522273656559, 1.341768146560826214, 0.3474236500605662470 ) ) ;
#3920=DIRECTION ( 'NONE',  ( -1.000000000000000000, 0.000000000000000000, 0.000000000000000000 ) ) ;
#3922=ORIENTED_EDGE ( 'NONE', *, *, #10347, .T. ) ;
#3923=ORIENTED_EDGE ( 'NONE', *, *, #9756, .F. ) ;
#3927=DIRECTION ( 'NONE',  ( 0.000000000000000000, 1.000000000000000000, 0.000000000000000000 ) ) ;
#3931=PLANE ( 'NONE',  #13392 ) ;
#3933=CARTESIAN_POINT ( 'NONE',  ( 7.232166136696967594E-17, 0.000000000000000000, 0.5905511811023621549 ) ) ;
#3936=TOROIDAL_SURFACE ( 'NONE', #10933, 0.6614173228346456046, 0.007874015748031495954 ) ;
#3945=ORIENTED_EDGE ( 'NONE', *, *, #15043, .F. ) ;
#3955=CARTESIAN_POINT ( 'NONE',  ( 7.232166136696967594E-17, 1.370078740157480546, 0.5905511811023621549 ) ) ;
#3956=CYLINDRICAL_SURFACE ( 'NONE', #8398, 0.5905511811023621549 ) ;
#3960=EDGE_CURVE ( 'NONE', #8067, #10377, #3296, .T. ) ;
#3961=DIRECTION ( 'NONE',  ( 0.8660254037844362651, 0.000000000000000000, -0.5000000000000041078 ) ) ;
#3965=DIRECTION ( 'NONE',  ( 0.000000000000000000, 0.000000000000000000, 1.000000000000000000 ) ) ;
#3968=AXIS2_PLACEMENT_3D ( 'NONE', #7123, #3603, #9320 ) ;
#3970=LINE ( 'NONE', #8905, #9357 ) ;
#3972=DIRECTION ( 'NONE',  ( 0.000000000000000000, 0.000000000000000000, 1.000000000000000000 ) ) ;
#3975=DIRECTION ( 'NONE',  ( 0.000000000000000000, 0.000000000000000000, -1.000000000000000000 ) ) ;
#3980=DIRECTION ( 'NONE',  ( 0.000000000000000000, 0.000000000000000000, -1.000000000000000000 ) ) ;
#3982=EDGE_CURVE ( 'NONE', #12461, #692, #6837, .T. ) ;
#3983=ORIENTED_EDGE ( 'NONE', *, *, #15011, .T. ) ;
#3991=FACE_OUTER_BOUND ( 'NONE', #4826, .T. ) ;
#3992=CARTESIAN_POINT ( 'NONE',  ( 0.000000000000000000, 1.645669291338583085, -0.7086614173228346081 ) ) ;
#3998=ADVANCED_FACE ( 'NONE', ( #7835 ), #1898, .F. ) ;
#3999=DIRECTION ( 'NONE',  ( -0.000000000000000000, -1.000000000000000000, -0.000000000000000000 ) ) ;
#4001=EDGE_LOOP ( 'NONE', ( #7465, #8050, #13852, #3492 ) ) ;
#4011=CARTESIAN_POINT ( 'NONE',  ( 0.7205731843802273273, 1.190944881889763884, 0.4842140986486808130 ) ) ;
#4017=CARTESIAN_POINT ( 'NONE',  ( 0.05905511811023622659, 1.043307086614173151, -0.8267716535433072833 ) ) ;
#4020=DIRECTION ( 'NONE',  ( 8.673617379884028076E-17, 1.000000000000000000, 0.000000000000000000 ) ) ;
#4027=ORIENTED_EDGE ( 'NONE', *, *, #11140, .F. ) ;
#4035=DIRECTION ( 'NONE',  ( -0.000000000000000000, -1.000000000000000000, -0.000000000000000000 ) ) ;
#4043=EDGE_CURVE ( 'NONE', #1436, #563, #8241, .T. ) ;
#4046=EDGE_CURVE ( 'NONE', #13544, #9837, #4545, .T. ) ;
#4053=CARTESIAN_POINT ( 'NONE',  ( 0.000000000000000000, 2.433070866141732846, 0.000000000000000000 ) ) ;
#4055=CARTESIAN_POINT ( 'NONE',  ( 0.000000000000000000, 1.606299212598425674, -0.6692913385826770867 ) ) ;
#4056=CARTESIAN_POINT ( 'NONE',  ( 0.000000000000000000, 2.433070866141732846, -0.5826771653543306728 ) ) ;
#4060=CARTESIAN_POINT ( 'NONE',  ( 0.000000000000000000, 0.5905511811023621549, 0.000000000000000000 ) ) ;
#4063=ADVANCED_FACE ( 'NONE', ( #15259 ), #12097, .F. ) ;
#4065=EDGE_LOOP ( 'NONE', ( #3945, #7797, #8415, #10493 ) ) ;
#4067=EDGE_CURVE ( 'NONE', #14427, #6389, #12598, .T. ) ;
#4069=DIRECTION ( 'NONE',  ( 0.000000000000000000, 0.000000000000000000, -1.000000000000000000 ) ) ;
#4072=CARTESIAN_POINT ( 'NONE',  ( 0.5445274672588121812, 1.338626482899105241, 0.2461921031270739857 ) ) ;
#4074=FACE_OUTER_BOUND ( 'NONE', #4736, .T. ) ;
#4078=AXIS2_PLACEMENT_3D ( 'NONE', #615, #6182, #12163 ) ;
#4079=AXIS2_PLACEMENT_3D ( 'NONE', #4502, #14064, #8333 ) ;
#4080=CARTESIAN_POINT ( 'NONE',  ( -0.4828087445803670441, 1.339342401112374903, 0.3474236500605482614 ) ) ;
#4081=AXIS2_PLACEMENT_3D ( 'NONE', #5676, #9291, #14155 ) ;
#4083=AXIS2_PLACEMENT_3D ( 'NONE', #10799, #12458, #14880 ) ;
#4084=ORIENTED_EDGE ( 'NONE', *, *, #3429, .T. ) ;
#4085=B_SPLINE_CURVE_WITH_KNOTS ( 'NONE', 3,
 ( #4451, #15031, #12823, #4281 ),
 .UNSPECIFIED., .F., .F.,
 ( 4, 4 ),
 ( 1.734723475976807094E-18, 2.119993237936608501E-05 ),
 .UNSPECIFIED. ) ;
#4089=DIRECTION ( 'NONE',  ( 0.5000000000000041078, -0.000000000000000000, 0.8660254037844363761 ) ) ;
#4090=CIRCLE ( 'NONE', #12611, 0.5905511811023621549 ) ;
#4091=AXIS2_PLACEMENT_3D ( 'NONE', #4340, #9140, #1844 ) ;
#4096=DIRECTION ( 'NONE',  ( -0.000000000000000000, -0.000000000000000000, 1.000000000000000000 ) ) ;
#4103=CIRCLE ( 'NONE', #4342, 0.007874015748031482076 ) ;
#4105=FACE_OUTER_BOUND ( 'NONE', #6408, .T. ) ;
#4106=AXIS2_PLACEMENT_3D ( 'NONE', #1957, #2895, #5532 ) ;
#4108=CIRCLE ( 'NONE', #3615, 0.03937007874015761161 ) ;
#4111=DIRECTION ( 'NONE',  ( -0.000000000000000000, -1.000000000000000000, 0.000000000000000000 ) ) ;
#4115=DIRECTION ( 'NONE',  ( 0.000000000000000000, -1.000000000000000000, 0.000000000000000000 ) ) ;
#4117=CARTESIAN_POINT ( 'NONE',  ( 0.4751993499420012479, 1.035433070866141891, 0.3506226965216235336 ) ) ;
#4122=LINE ( 'NONE', #1849, #10328 ) ;
#4131=AXIS2_PLACEMENT_3D ( 'NONE', #7207, #13301, #10732 ) ;
#4139=LINE ( 'NONE', #6544, #9348 ) ;
#4142=VECTOR ( 'NONE', #13064, 39.37007874015748143 ) ;
#4150=EDGE_LOOP ( 'NONE', ( #4768, #11696, #4789, #3516 ) ) ;
#4151=VECTOR ( 'NONE', #14995, 39.37007874015748143 ) ;
#4153=AXIS2_PLACEMENT_3D ( 'NONE', #10288, #1595, #14928 ) ;
#4154=CARTESIAN_POINT ( 'NONE',  ( 0.000000000000000000, 1.346456692913385877, 0.000000000000000000 ) ) ;
#4159=EDGE_CURVE ( 'NONE', #5321, #562, #11878, .T. ) ;
#4168=CIRCLE ( 'NONE', #7928, 0.03937007874015751446 ) ;
#4173=DIRECTION ( 'NONE',  ( 0.000000000000000000, 0.000000000000000000, -1.000000000000000000 ) ) ;
#4176=DIRECTION ( 'NONE',  ( -0.000000000000000000, -1.000000000000000000, -0.000000000000000000 ) ) ;
#4179=DIRECTION ( 'NONE',  ( 0.000000000000000000, 0.000000000000000000, 1.000000000000000000 ) ) ;
#4184=DIRECTION ( 'NONE',  ( 0.000000000000000000, 1.000000000000000000, 0.000000000000000000 ) ) ;
#4193=EDGE_LOOP ( 'NONE', ( #4587, #12288, #1894, #11439 ) ) ;
#4195=CARTESIAN_POINT ( 'NONE',  ( 0.000000000000000000, 0.5826771653543306728, -0.7007874015748031260 ) ) ;
#4198=DIRECTION ( 'NONE',  ( 1.000000000000000000, 0.000000000000000000, 0.000000000000000000 ) ) ;
#4199=MANIFOLD_SOLID_BREP ( 'Fillet2', #630 ) ;
#4206=ORIENTED_EDGE ( 'NONE', *, *, #14724, .F. ) ;
#4207=AXIS2_PLACEMENT_3D ( 'NONE', #4232, #9020, #10332 ) ;
#4209=ORIENTED_EDGE ( 'NONE', *, *, #15043, .T. ) ;
#4217=DIRECTION ( 'NONE',  ( -0.000000000000000000, -1.000000000000000000, -0.000000000000000000 ) ) ;
#4222=CARTESIAN_POINT ( 'NONE',  ( -0.5905511811023621549, 2.440944881889763884, -0.04724409448818898266 ) ) ;
#4226=ADVANCED_FACE ( 'NONE', ( #15318, #8563 ), #5254, .T. ) ;
#4230=DIRECTION ( 'NONE',  ( 0.000000000000000000, 0.000000000000000000, -1.000000000000000000 ) ) ;
#4231=DIRECTION ( 'NONE',  ( 0.000000000000000000, 0.000000000000000000, 1.000000000000000000 ) ) ;
#4232=CARTESIAN_POINT ( 'NONE',  ( 0.000000000000000000, 2.440944881889763884, 0.000000000000000000 ) ) ;
#4236=CARTESIAN_POINT ( 'NONE',  ( 0.000000000000000000, 1.385826771653543510, 0.000000000000000000 ) ) ;
#4241=ORIENTED_EDGE ( 'NONE', *, *, #9033, .T. ) ;
#4260=ORIENTED_EDGE ( 'NONE', *, *, #260, .F. ) ;
#4264=DIRECTION ( 'NONE',  ( 0.000000000000000000, 0.000000000000000000, 1.000000000000000000 ) ) ;
#4278=CARTESIAN_POINT ( 'NONE',  ( 0.000000000000000000, 1.425196850393700920, -0.6692913385826770867 ) ) ;
#4279=LINE ( 'NONE', #9067, #15119 ) ;
#4281=CARTESIAN_POINT ( 'NONE',  ( 0.05905511811023622659, 1.338626482899105241, -0.5946706712680680518 ) ) ;
#4282=CARTESIAN_POINT ( 'NONE',  ( 0.000000000000000000, 0.5511811023622046335, 0.000000000000000000 ) ) ;
#4290=EDGE_LOOP ( 'NONE', ( #11419, #2348, #10012, #14808 ) ) ;
#4295=CARTESIAN_POINT ( 'NONE',  ( -0.4841913566216235476, 1.043107366814280734, 0.3477389867607276752 ) ) ;
#4301=CARTESIAN_POINT ( 'NONE',  ( 0.000000000000000000, 0.5905511811023621549, 0.000000000000000000 ) ) ;
#4306=ORIENTED_EDGE ( 'NONE', *, *, #9756, .T. ) ;
#4307=EDGE_CURVE ( 'NONE', #9168, #11283, #8602, .T. ) ;
#4310=CARTESIAN_POINT ( 'NONE',  ( 0.000000000000000000, 1.409448818897637956, -0.5511811023622046335 ) ) ;
#4321=EDGE_CURVE ( 'NONE', #25, #7594, #12613, .T. ) ;
#4325=CARTESIAN_POINT ( 'NONE',  ( 8.148240514011916814E-17, 1.614173228346457156, -0.6614173228346456046 ) ) ;
#4328=ADVANCED_FACE ( 'NONE', ( #12387 ), #1348, .F. ) ;
#4329=CARTESIAN_POINT ( 'NONE',  ( 0.000000000000000000, 0.5905511811023621549, 0.000000000000000000 ) ) ;
#4331=EDGE_LOOP ( 'NONE', ( #185, #2308, #7908, #363 ) ) ;
#4332=AXIS2_PLACEMENT_3D ( 'NONE', #211, #12099, #12261 ) ;
#4333=VERTEX_POINT ( 'NONE', #2674 ) ;
#4339=DIRECTION ( 'NONE',  ( -0.8660254037844433705, 0.000000000000000000, -0.4999999999999918954 ) ) ;
#4340=CARTESIAN_POINT ( 'NONE',  ( 0.000000000000000000, 1.614173228346457156, 0.000000000000000000 ) ) ;
#4342=AXIS2_PLACEMENT_3D ( 'NONE', #7077, #5904, #4799 ) ;
#4345=AXIS2_PLACEMENT_3D ( 'NONE', #6130, #7587, #1660 ) ;
#4346=CARTESIAN_POINT ( 'NONE',  ( 0.4815353412745266848, 1.041793866378536437, 0.3474236500605469291 ) ) ;
#4349=VECTOR ( 'NONE', #4020, 39.37007874015748143 ) ;
#4351=EDGE_CURVE ( 'NONE', #4716, #6519, #10609, .T. ) ;
#4355=ORIENTED_EDGE ( 'NONE', *, *, #12900, .F. ) ;
#4368=ORIENTED_EDGE ( 'NONE', *, *, #14866, .T. ) ;
#4375=EDGE_LOOP ( 'NONE', ( #14133, #1965, #9782, #3817, #6684, #3361 ) ) ;
#4383=AXIS2_PLACEMENT_3D ( 'NONE', #10729, #10, #4837 ) ;
#4387=DIRECTION ( 'NONE',  ( -0.000000000000000000, -1.000000000000000000, -0.000000000000000000 ) ) ;
#4388=VECTOR ( 'NONE', #8501, 39.37007874015747433 ) ;
#4390=EDGE_LOOP ( 'NONE', ( #13169, #6390, #8706, #3766 ) ) ;
#4397=AXIS2_PLACEMENT_3D ( 'NONE', #12489, #6504, #5249 ) ;
#4411=CARTESIAN_POINT ( 'NONE',  ( 0.06604848736013263499, 0.000000000000000000, -0.5868460571724355423 ) ) ;
#4412=EDGE_LOOP ( 'NONE', ( #12693, #11256 ) ) ;
#4413=CARTESIAN_POINT ( 'NONE',  ( 0.000000000000000000, 2.401574803149606918, 0.000000000000000000 ) ) ;
#4415=CIRCLE ( 'NONE', #3178, 0.5905511811023621549 ) ;
#4416=PLANE ( 'NONE',  #11708 ) ;
#4422=CIRCLE ( 'NONE', #1679, 0.7086614173228346081 ) ;
#4424=EDGE_CURVE ( 'NONE', #8620, #1922, #3848, .T. ) ;
#4428=CARTESIAN_POINT ( 'NONE',  ( -0.7455328141524873997, 1.190944881889763884, 0.3622425942647021779 ) ) ;
#4429=AXIS2_PLACEMENT_3D ( 'NONE', #6508, #12730, #13810 ) ;
#4430=FACE_OUTER_BOUND ( 'NONE', #7180, .T. ) ;
#4433=CIRCLE ( 'NONE', #13198, 0.1574803149606299191 ) ;
#4438=CIRCLE ( 'NONE', #936, 0.5826771653543306728 ) ;
#4445=AXIS2_PLACEMENT_3D ( 'NONE', #6692, #13685, #8987 ) ;
#4446=EDGE_CURVE ( 'NONE', #14049, #7994, #12380, .T. ) ;
#4451=CARTESIAN_POINT ( 'NONE',  ( 0.05905511811023622659, 1.338582677165354395, -0.5955041639236611228 ) ) ;
#4456=VERTEX_POINT ( 'NONE', #12307 ) ;
#4460=EDGE_LOOP ( 'NONE', ( #1995, #10417, #7267, #8920 ) ) ;
#4461=ORIENTED_EDGE ( 'NONE', *, *, #11912, .F. ) ;
#4465=CIRCLE ( 'NONE', #13981, 0.007874015748031516770 ) ;
#4468=ADVANCED_FACE ( 'NONE', ( #1565, #6324 ), #11124, .T. ) ;
#4469=FACE_OUTER_BOUND ( 'NONE', #3172, .T. ) ;
#4473=DIRECTION ( 'NONE',  ( 1.224646799147343593E-16, 0.000000000000000000, -1.000000000000000000 ) ) ;
#4478=FACE_OUTER_BOUND ( 'NONE', #12423, .T. ) ;
#4480=EDGE_LOOP ( 'NONE', ( #12762, #13832, #11259, #10412 ) ) ;
#4489=EDGE_LOOP ( 'NONE', ( #7632, #1425, #1319, #7884 ) ) ;
#4502=CARTESIAN_POINT ( 'NONE',  ( -0.6864776960422505070, 1.190944881889763884, 0.4645290592786119332 ) ) ;
#4507=ADVANCED_FACE ( 'NONE', ( #2029 ), #12617, .F. ) ;
#4515=EDGE_CURVE ( 'NONE', #2422, #6453, #5604, .T. ) ;
#4532=EDGE_CURVE ( 'NONE', #8791, #15270, #3115, .T. ) ;
#4533=ORIENTED_EDGE ( 'NONE', *, *, #10975, .F. ) ;
#4535=CARTESIAN_POINT ( 'NONE',  ( -0.05905511811023622659, 1.190944881889763884, -0.8661417322834648047 ) ) ;
#4540=VERTEX_POINT ( 'NONE', #5539 ) ;
#4542=CARTESIAN_POINT ( 'NONE',  ( -0.05905511811023622659, 1.338877451511696792, -0.5922897223582481718 ) ) ;
#4545=LINE ( 'NONE', #4712, #14845 ) ;
#4548=VERTEX_POINT ( 'NONE', #4535 ) ;
#4552=ORIENTED_EDGE ( 'NONE', *, *, #3176, .T. ) ;
#4553=CARTESIAN_POINT ( 'NONE',  ( 0.000000000000000000, 1.614173228346457156, 0.000000000000000000 ) ) ;
#4557=CARTESIAN_POINT ( 'NONE',  ( -0.05905511811023622659, 1.043263280880422528, -0.5946706712680680518 ) ) ;
#4573=CIRCLE ( 'NONE', #11070, 0.5590551181102362266 ) ;
#4581=CARTESIAN_POINT ( 'NONE',  ( 6.846450609406462919E-17, 1.409448818897637956, 0.5590551181102362266 ) ) ;
#4586=ORIENTED_EDGE ( 'NONE', *, *, #15440, .F. ) ;
#4587=ORIENTED_EDGE ( 'NONE', *, *, #4446, .T. ) ;
#4589=ORIENTED_EDGE ( 'NONE', *, *, #4351, .T. ) ;
#4590=EDGE_LOOP ( 'NONE', ( #12988, #7282, #1812, #6801, #11342 ) ) ;
#4605=ORIENTED_EDGE ( 'NONE', *, *, #2432, .F. ) ;
#4609=TOROIDAL_SURFACE ( 'NONE', #4106, 0.5984251968503937480, 0.007874015748031495954 ) ;
#4611=AXIS2_PLACEMENT_3D ( 'NONE', #8079, #12867, #12952 ) ;
#4614=EDGE_CURVE ( 'NONE', #14592, #851, #3184, .T. ) ;
#4615=EDGE_CURVE ( 'NONE', #4540, #1832, #3623, .T. ) ;
#4618=CARTESIAN_POINT ( 'NONE',  ( -0.1181102362204724532, 2.637795275590551825, 0.03937007874015747977 ) ) ;
#4619=AXIS2_PLACEMENT_3D ( 'NONE', #10751, #6028, #9811 ) ;
#4624=ORIENTED_EDGE ( 'NONE', *, *, #11729, .T. ) ;
#4627=DIRECTION ( 'NONE',  ( -0.000000000000000000, -1.000000000000000000, -0.000000000000000000 ) ) ;
#4629=CARTESIAN_POINT ( 'NONE',  ( 0.4815353412745612127, 0.000000000000000000, 0.3474236500605469846 ) ) ;
#4630=CARTESIAN_POINT ( 'NONE',  ( -0.5412478373021294420, 0.000000000000000000, 0.2362233606508100381 ) ) ;
#4638=TOROIDAL_SURFACE ( 'NONE', #14656, 0.7007874015748031260, 0.007874015748031495954 ) ;
#4654=CYLINDRICAL_SURFACE ( 'NONE', #12955, 0.1476377952755906220 ) ;
#4672=FACE_OUTER_BOUND ( 'NONE', #4065, .T. ) ;
#4673=CARTESIAN_POINT ( 'NONE',  ( -0.1181102362204724254, 2.448818897637795367, 0.03937007874015747977 ) ) ;
#4680=ORIENTED_EDGE ( 'NONE', *, *, #5493, .F. ) ;
#4687=DIRECTION ( 'NONE',  ( 1.224646799147353947E-16, 0.000000000000000000, -1.000000000000000000 ) ) ;
#4689=DIRECTION ( 'NONE',  ( -0.000000000000000000, -1.000000000000000000, -0.000000000000000000 ) ) ;
#4690=CARTESIAN_POINT ( 'NONE',  ( -0.5445274672588088505, 1.338626482899105241, 0.2461921031270815630 ) ) ;
#4695=DIRECTION ( 'NONE',  ( 0.000000000000000000, 0.000000000000000000, -1.000000000000000000 ) ) ;
#4698=ORIENTED_EDGE ( 'NONE', *, *, #15142, .T. ) ;
#4699=AXIS2_PLACEMENT_3D ( 'NONE', #15097, #9004, #2970 ) ;
#4704=CARTESIAN_POINT ( 'NONE',  ( 7.328595018519593763E-17, 0.3070866141732283561, -0.5984251968503937480 ) ) ;
#4712=CARTESIAN_POINT ( 'NONE',  ( 0.6864776960422567242, 1.338582677165354395, 0.4645290592786021633 ) ) ;
#4716=VERTEX_POINT ( 'NONE', #81 ) ;
#4722=CYLINDRICAL_SURFACE ( 'NONE', #12834, 0.5511811023622046335 ) ;
#4723=CIRCLE ( 'NONE', #6202, 0.1181102362204724532 ) ;
#4725=CARTESIAN_POINT ( 'NONE',  ( -0.05905511811023624047, 1.043307086614173373, -0.5952259495879738127 ) ) ;
#4729=CARTESIAN_POINT ( 'NONE',  ( 8.148240514011916814E-17, 0.3543307086614172485, 0.6614173228346456046 ) ) ;
#4730=CARTESIAN_POINT ( 'NONE',  ( 0.6523822077042866763, 1.190944881889763884, 0.4448440199085238467 ) ) ;
#4731=ADVANCED_FACE ( 'NONE', ( #1024 ), #6082, .F. ) ;
#4736=EDGE_LOOP ( 'NONE', ( #2280, #3519, #13081, #14432 ) ) ;
#4740=EDGE_CURVE ( 'NONE', #7046, #10377, #9874, .T. ) ;
#4749=CARTESIAN_POINT ( 'NONE',  ( 8.630384923125046426E-17, 0.3149606299212598381, -0.7007874015748031260 ) ) ;
#4751=ORIENTED_EDGE ( 'NONE', *, *, #6055, .T. ) ;
#4752=ORIENTED_EDGE ( 'NONE', *, *, #10931, .T. ) ;
#4754=EDGE_CURVE ( 'NONE', #5666, #5246, #11554, .T. ) ;
#4755=ADVANCED_FACE ( 'NONE', ( #13534, #12291 ), #7430, .F. ) ;
#4760=PLANE ( 'NONE',  #11839 ) ;
#4763=FACE_OUTER_BOUND ( 'NONE', #760, .T. ) ;
#4766=ORIENTED_EDGE ( 'NONE', *, *, #11607, .T. ) ;
#4767=ORIENTED_EDGE ( 'NONE', *, *, #4515, .T. ) ;
#4768=ORIENTED_EDGE ( 'NONE', *, *, #9328, .T. ) ;
#4780=CARTESIAN_POINT ( 'NONE',  ( 0.5412723129863803440, 1.340161119985692428, 0.2430722610364096370 ) ) ;
#4781=ORIENTED_EDGE ( 'NONE', *, *, #424, .T. ) ;
#4782=EDGE_LOOP ( 'NONE', ( #1855, #7764, #11399, #9027, #5505, #3787, #12199 ) ) ;
#4789=ORIENTED_EDGE ( 'NONE', *, *, #9273, .F. ) ;
#4795=EDGE_LOOP ( 'NONE', ( #6233, #6996, #8326, #578 ) ) ;
#4799=DIRECTION ( 'NONE',  ( 0.000000000000000000, 0.000000000000000000, 1.000000000000000000 ) ) ;
#4804=ADVANCED_FACE ( 'NONE', ( #5059 ), #7349, .F. ) ;
#4807=CARTESIAN_POINT ( 'NONE',  ( 6.846450609406462919E-17, 1.622047244094488638, -0.5590551181102362266 ) ) ;
#4808=DIRECTION ( 'NONE',  ( -0.000000000000000000, -1.000000000000000000, -0.000000000000000000 ) ) ;
#4815=ORIENTED_EDGE ( 'NONE', *, *, #2835, .T. ) ;
#4817=CARTESIAN_POINT ( 'NONE',  ( 0.000000000000000000, 2.433070866141732846, 0.000000000000000000 ) ) ;
#4822=CARTESIAN_POINT ( 'NONE',  ( 0.000000000000000000, 0.3070866141732283561, -0.5905511811023621549 ) ) ;
#4823=AXIS2_PLACEMENT_3D ( 'NONE', #13089, #11939, #2356 ) ;
#4825=CARTESIAN_POINT ( 'NONE',  ( 0.000000000000000000, 1.622047244094488638, 0.000000000000000000 ) ) ;
#4826=EDGE_LOOP ( 'NONE', ( #14973, #8035, #4766, #4880 ) ) ;
#4832=ORIENTED_EDGE ( 'NONE', *, *, #6413, .T. ) ;
#4834=ORIENTED_EDGE ( 'NONE', *, *, #12581, .F. ) ;
#4835=AXIS2_PLACEMENT_3D ( 'NONE', #8351, #7184, #7407 ) ;
#4837=DIRECTION ( 'NONE',  ( 0.000000000000000000, 0.000000000000000000, 1.000000000000000000 ) ) ;
#4848=EDGE_CURVE ( 'NONE', #3695, #8997, #366, .T. ) ;
#4855=VECTOR ( 'NONE', #773, 39.37007874015748143 ) ;
#4857=EDGE_CURVE ( 'NONE', #11091, #14143, #11108, .T. ) ;
#4860=DIRECTION ( 'NONE',  ( -0.000000000000000000, 1.000000000000000000, -0.000000000000000000 ) ) ;
#4865=DIRECTION ( 'NONE',  ( -0.000000000000000000, -1.000000000000000000, -0.000000000000000000 ) ) ;
#4879=ORIENTED_EDGE ( 'NONE', *, *, #2157, .T. ) ;
#4880=ORIENTED_EDGE ( 'NONE', *, *, #6451, .T. ) ;
#4886=CARTESIAN_POINT ( 'NONE',  ( 0.000000000000000000, 0.000000000000000000, -0.5905511811023621549 ) ) ;
#4888=TOROIDAL_SURFACE ( 'NONE', #7153, 0.7007874015748031260, 0.007874015748031495954 ) ;
#4893=CARTESIAN_POINT ( 'NONE',  ( 0.000000000000000000, 0.000000000000000000, 0.000000000000000000 ) ) ;
#4894=CARTESIAN_POINT ( 'NONE',  ( 7.328595018519593763E-17, 1.653543307086614567, 0.5984251968503937480 ) ) ;
#4899=DIRECTION ( 'NONE',  ( 0.5000000000000041078, 0.000000000000000000, 0.8660254037844362651 ) ) ;
#4905=AXIS2_PLACEMENT_3D ( 'NONE', #11397, #449, #3965 ) ;
#4914=AXIS2_PLACEMENT_3D ( 'NONE', #2477, #354, #11067 ) ;
#4915=CARTESIAN_POINT ( 'NONE',  ( 6.750021727583836750E-17, 0.04724409448818898960, 0.5511811023622046335 ) ) ;
#4918=DIRECTION ( 'NONE',  ( 8.673617379884028076E-17, -1.000000000000000000, 0.000000000000000000 ) ) ;
#4934=CARTESIAN_POINT ( 'NONE',  ( 0.000000000000000000, 0.03149606299212599769, 0.000000000000000000 ) ) ;
#4938=DIRECTION ( 'NONE',  ( -0.000000000000000000, -1.000000000000000000, 4.956352788505160310E-16 ) ) ;
#4939=CARTESIAN_POINT ( 'NONE',  ( 0.5403775459648877399, 1.343094183513034778, 0.2394881783597540836 ) ) ;
#4943=ORIENTED_EDGE ( 'NONE', *, *, #4307, .T. ) ;
#4945=EDGE_CURVE ( 'NONE', #1542, #14687, #4085, .T. ) ;
#4947=CARTESIAN_POINT ( 'NONE',  ( 8.678599364036360127E-17, 0.5826771653543306728, 0.7086614173228346081 ) ) ;
#4954=EDGE_CURVE ( 'NONE', #3736, #2187, #112, .T. ) ;
#4963=DIRECTION ( 'NONE',  ( -0.000000000000000000, -1.000000000000000000, 0.000000000000000000 ) ) ;
#4966=( NAMED_UNIT ( * ) SI_UNIT ( $, .STERADIAN. ) SOLID_ANGLE_UNIT ( ) );
#4967=LINE ( 'NONE', #6046, #14868 ) ;
#4973=ORIENTED_EDGE ( 'NONE', *, *, #7023, .F. ) ;
#4978=EDGE_CURVE ( 'NONE', #8620, #12332, #13250, .T. ) ;
#4984=CARTESIAN_POINT ( 'NONE',  ( 0.4861941749621881415, 1.043307086614173373, 0.3488953144687809704 ) ) ;
#4991=CARTESIAN_POINT ( 'NONE',  ( 7.328595018519593763E-17, 0.3149606299212598381, -0.5984251968503937480 ) ) ;
#4994=CARTESIAN_POINT ( 'NONE',  ( 8.100026073100603114E-17, 1.425196850393700920, 0.6614173228346456046 ) ) ;
#5006=EDGE_LOOP ( 'NONE', ( #8806, #8260, #14475, #4552 ) ) ;
#5007=DIRECTION ( 'NONE',  ( 0.000000000000000000, 0.000000000000000000, 1.000000000000000000 ) ) ;
#5008=CARTESIAN_POINT ( 'NONE',  ( 0.000000000000000000, 0.5433070866141731514, 0.000000000000000000 ) ) ;
#5009=DIRECTION ( 'NONE',  ( 0.000000000000000000, 1.000000000000000000, -0.000000000000000000 ) ) ;
#5012=CARTESIAN_POINT ( 'NONE',  ( 0.7455328141524921737, 1.190944881889763884, 0.3622425942646917418 ) ) ;
#5013=EDGE_CURVE ( 'NONE', #4456, #2187, #9615, .T. ) ;
#5019=EDGE_CURVE ( 'NONE', #13544, #7994, #4967, .T. ) ;
#5023=ORIENTED_EDGE ( 'NONE', *, *, #4424, .F. ) ;
#5027=CARTESIAN_POINT ( 'NONE',  ( 0.000000000000000000, 0.5511811023622046335, 0.000000000000000000 ) ) ;
#5032=CARTESIAN_POINT ( 'NONE',  ( -0.7455328141524870667, 1.338582677165354395, 0.3622425942647020669 ) ) ;
#5034=CARTESIAN_POINT ( 'NONE',  ( 0.000000000000000000, 1.370078740157480546, 0.5984251968503937480 ) ) ;
#5045=DIRECTION ( 'NONE',  ( 0.000000000000000000, 0.000000000000000000, 1.000000000000000000 ) ) ;
#5052=VERTEX_POINT ( 'NONE', #10483 ) ;
#5053=ORIENTED_EDGE ( 'NONE', *, *, #10364, .T. ) ;
#5056=AXIS2_PLACEMENT_3D ( 'NONE', #231, #2779, #14482 ) ;
#5059=FACE_OUTER_BOUND ( 'NONE', #13105, .T. ) ;
#5062=CARTESIAN_POINT ( 'NONE',  ( 0.06604848736013260724, 1.035433070866141891, -0.5868460571724354313 ) ) ;
#5066=LINE ( 'NONE', #4222, #14450 ) ;
#5070=VERTEX_POINT ( 'NONE', #8132 ) ;
#5078=ADVANCED_FACE ( 'NONE', ( #5690 ), #14116, .F. ) ;
#5079=DIRECTION ( 'NONE',  ( -0.4999999999999919509, 0.000000000000000000, 0.8660254037844432595 ) ) ;
#5092=DIRECTION ( 'NONE',  ( -0.000000000000000000, 1.000000000000000000, 0.000000000000000000 ) ) ;
#5105=AXIS2_PLACEMENT_3D ( 'NONE', #4994, #3601, #14561 ) ;
#5112=CARTESIAN_POINT ( 'NONE',  ( -0.1259842519685039353, 2.440944881889763884, 0.04724409448818898266 ) ) ;
#5115=VECTOR ( 'NONE', #5654, 39.37007874015748143 ) ;
#5117=CIRCLE ( 'NONE', #1140, 0.5511811023622046335 ) ;
#5118=DIRECTION ( 'NONE',  ( -1.000000000000000000, 0.000000000000000000, 0.000000000000000000 ) ) ;
#5121=ORIENTED_EDGE ( 'NONE', *, *, #10213, .F. ) ;
#5132=CARTESIAN_POINT ( 'NONE',  ( 0.4787089944775337336, 1.040121464703355425, 0.3474236500605593636 ) ) ;
#5136=DIRECTION ( 'NONE',  ( 1.000000000000000000, 0.000000000000000000, -1.224646799147353207E-16 ) ) ;
#5137=ADVANCED_FACE ( 'NONE', ( #8425 ), #12191, .F. ) ;
#5138=CARTESIAN_POINT ( 'NONE',  ( 0.06440205152080440143, 1.344788853693112962, -0.5870313606185335598 ) ) ;
#5141=CIRCLE ( 'NONE', #13909, 0.5511811023622046335 ) ;
#5146=ORIENTED_EDGE ( 'NONE', *, *, #12303, .F. ) ;
#5152=CARTESIAN_POINT ( 'NONE',  ( 0.000000000000000000, 2.440944881889763884, 0.000000000000000000 ) ) ;
#5153=CARTESIAN_POINT ( 'NONE',  ( 0.05905511811023625435, 2.637795275590551825, -0.03937007874015747977 ) ) ;
#5163=DIRECTION ( 'NONE',  ( 0.000000000000000000, 0.000000000000000000, -1.000000000000000000 ) ) ;
#5166=ORIENTED_EDGE ( 'NONE', *, *, #10276, .F. ) ;
#5172=CARTESIAN_POINT ( 'NONE',  ( -0.4815353412745217998, 1.340095897400991110, 0.3474236500605538125 ) ) ;
#5179=EDGE_LOOP ( 'NONE', ( #1240, #11870 ) ) ;
#5180=CARTESIAN_POINT ( 'NONE',  ( 0.000000000000000000, 1.385826771653543510, -0.7086614173228346081 ) ) ;
#5182=TOROIDAL_SURFACE ( 'NONE', #8209, 0.1653543307086614012, 0.007874015748031495954 ) ;
#5187=EDGE_CURVE ( 'NONE', #6857, #15219, #7625, .T. ) ;
#5188=FACE_OUTER_BOUND ( 'NONE', #3854, .T. ) ;
#5195=VERTEX_POINT ( 'NONE', #3955 ) ;
#5200=ORIENTED_EDGE ( 'NONE', *, *, #7107, .T. ) ;
#5201=AXIS2_PLACEMENT_3D ( 'NONE', #541, #2887, #7742 ) ;
#5220=EDGE_CURVE ( 'NONE', #12883, #13266, #8380, .T. ) ;
#5223=CARTESIAN_POINT ( 'NONE',  ( 0.000000000000000000, 0.04724409448818898960, 0.000000000000000000 ) ) ;
#5230=DIRECTION ( 'NONE',  ( 0.000000000000000000, 1.000000000000000000, 0.000000000000000000 ) ) ;
#5236=DIRECTION ( 'NONE',  ( -0.000000000000000000, -1.000000000000000000, -0.000000000000000000 ) ) ;
#5237=FACE_BOUND ( 'NONE', #11484, .T. ) ;
#5241=DIRECTION ( 'NONE',  ( 0.000000000000000000, 0.000000000000000000, 1.000000000000000000 ) ) ;
#5246=VERTEX_POINT ( 'NONE', #3074 ) ;
#5249=DIRECTION ( 'NONE',  ( 0.000000000000000000, 0.000000000000000000, -1.000000000000000000 ) ) ;
#5250=EDGE_CURVE ( 'NONE', #4540, #11532, #2935, .T. ) ;
#5254=CYLINDRICAL_SURFACE ( 'NONE', #2847, 0.5905511811023621549 ) ;
#5255=CARTESIAN_POINT ( 'NONE',  ( -0.7455328141524873997, 1.043307086614173151, 0.3622425942647021779 ) ) ;
#5261=ORIENTED_EDGE ( 'NONE', *, *, #6147, .F. ) ;
#5263=CARTESIAN_POINT ( 'NONE',  ( -0.5412478373021294420, 1.035433070866141891, 0.2362233606508100381 ) ) ;
#5275=DIRECTION ( 'NONE',  ( 0.000000000000000000, 0.000000000000000000, 1.000000000000000000 ) ) ;
#5278=ORIENTED_EDGE ( 'NONE', *, *, #10784, .T. ) ;
#5280=EDGE_LOOP ( 'NONE', ( #2828, #696 ) ) ;
#5282=EDGE_CURVE ( 'NONE', #697, #2543, #14834, .T. ) ;
#5289=CARTESIAN_POINT ( 'NONE',  ( 0.4765664223159776780, 1.344138844425384560, 0.3487699017371386212 ) ) ;
#5294=ORIENTED_EDGE ( 'NONE', *, *, #7781, .F. ) ;
#5296=DIRECTION ( 'NONE',  ( 0.000000000000000000, 0.000000000000000000, -1.000000000000000000 ) ) ;
#5297=DIRECTION ( 'NONE',  ( 1.000000000000000000, 0.000000000000000000, 0.000000000000000000 ) ) ;
#5299=ADVANCED_FACE ( 'NONE', ( #1522 ), #6274, .T. ) ;
#5300=ORIENTED_EDGE ( 'NONE', *, *, #3571, .T. ) ;
#5302=AXIS2_PLACEMENT_3D ( 'NONE', #8221, #1014, #10639 ) ;
#5306=EDGE_CURVE ( 'NONE', #2107, #12371, #13890, .T. ) ;
#5311=CARTESIAN_POINT ( 'NONE',  ( -0.5068643957866975081, 1.043307086614173373, 0.2244473186741497150 ) ) ;
#5321=VERTEX_POINT ( 'NONE', #5797 ) ;
#5323=ORIENTED_EDGE ( 'NONE', *, *, #14749, .T. ) ;
#5326=VECTOR ( 'NONE', #14710, 39.37007874015748143 ) ;
#5327=CIRCLE ( 'NONE', #2587, 0.7086614173228346081 ) ;
#5329=CARTESIAN_POINT ( 'NONE',  ( 6.846450609406462919E-17, 0.3543307086614172485, 0.5590551181102362266 ) ) ;
#5336=DIRECTION ( 'NONE',  ( 0.000000000000000000, 0.000000000000000000, -1.000000000000000000 ) ) ;
#5350=AXIS2_PLACEMENT_3D ( 'NONE', #6210, #3728, #7472 ) ;
#5354=VECTOR ( 'NONE', #10495, 39.37007874015748143 ) ;
#5361=DIRECTION ( 'NONE',  ( -0.000000000000000000, -1.000000000000000000, -0.000000000000000000 ) ) ;
#5369=AXIS2_PLACEMENT_3D ( 'NONE', #11117, #2608, #13338 ) ;
#5374=CARTESIAN_POINT ( 'NONE',  ( 0.000000000000000000, 1.645669291338583085, 0.000000000000000000 ) ) ;
#5380=DIRECTION ( 'NONE',  ( 1.000000000000000000, 0.000000000000000000, -1.224646799147353207E-16 ) ) ;
#5389=CIRCLE ( 'NONE', #7399, 0.7086614173228346081 ) ;
#5396=EDGE_LOOP ( 'NONE', ( #6986, #5465, #14721, #8520 ) ) ;
#5398=AXIS2_PLACEMENT_3D ( 'NONE', #2143, #7942, #1992 ) ;
#5399=B_SPLINE_CURVE_WITH_KNOTS ( 'NONE', 3,
 ( #9024, #2915, #10120, #728 ),
 .UNSPECIFIED., .F., .F.,
 ( 4, 4 ),
 ( 0.000000000000000000, 2.119993237936300859E-05 ),
 .UNSPECIFIED. ) ;
#5400=CARTESIAN_POINT ( 'NONE',  ( -0.4828087445803670441, 1.042547362667152644, 0.3474236500605482614 ) ) ;
#5401=PLANE ( 'NONE',  #11732 ) ;
#5406=AXIS2_PLACEMENT_3D ( 'NONE', #10368, #11624, #14217 ) ;
#5412=ORIENTED_EDGE ( 'NONE', *, *, #14823, .F. ) ;
#5423=TOROIDAL_SURFACE ( 'NONE', #7679, 0.5590551181102362266, 0.007874015748031495954 ) ;
#5441=DIRECTION ( 'NONE',  ( 1.000000000000000000, 0.000000000000000000, 0.000000000000000000 ) ) ;
#5443=FACE_OUTER_BOUND ( 'NONE', #6894, .T. ) ;
#5445=CARTESIAN_POINT ( 'NONE',  ( 0.000000000000000000, 0.000000000000000000, -0.6692913385826770867 ) ) ;
#5450=ORIENTED_EDGE ( 'NONE', *, *, #1388, .F. ) ;
#5452=AXIS2_PLACEMENT_3D ( 'NONE', #14025, #4387, #10734 ) ;
#5457=PLANE ( 'NONE',  #11376 ) ;
#5460=CARTESIAN_POINT ( 'NONE',  ( 7.135737254874341425E-17, 2.433070866141732846, 0.5826771653543306728 ) ) ;
#5461=DIRECTION ( 'NONE',  ( 0.8660254037844431485, -4.956352788505159323E-16, 0.4999999999999918954 ) ) ;
#5465=ORIENTED_EDGE ( 'NONE', *, *, #752, .F. ) ;
#5467=EDGE_CURVE ( 'NONE', #5735, #10243, #6360, .T. ) ;
#5468=CARTESIAN_POINT ( 'NONE',  ( -0.5445274672588088505, 1.338626482899105241, 0.2461921031270815630 ) ) ;
#5470=ORIENTED_EDGE ( 'NONE', *, *, #14303, .T. ) ;
#5472=DIRECTION ( 'NONE',  ( 0.000000000000000000, -0.000000000000000000, 1.000000000000000000 ) ) ;
#5476=CARTESIAN_POINT ( 'NONE',  ( -0.4859532342797812654, 1.043307086614173373, 0.3487562073009442543 ) ) ;
#5477=DIRECTION ( 'NONE',  ( -0.000000000000000000, -1.000000000000000000, -0.000000000000000000 ) ) ;
#5486=VERTEX_POINT ( 'NONE', #9747 ) ;
#5489=ORIENTED_EDGE ( 'NONE', *, *, #11299, .F. ) ;
#5490=EDGE_LOOP ( 'NONE', ( #10349, #1332, #14883, #6365, #3047 ) ) ;
#5492=LINE ( 'NONE', #14996, #6635 ) ;
#5493=EDGE_CURVE ( 'NONE', #2210, #6005, #9668, .T. ) ;
#5495=DIRECTION ( 'NONE',  ( 0.000000000000000000, -1.000000000000000000, 0.000000000000000000 ) ) ;
#5497=FACE_OUTER_BOUND ( 'NONE', #7818, .T. ) ;
#5499=ORIENTED_EDGE ( 'NONE', *, *, #2878, .T. ) ;
#5505=ORIENTED_EDGE ( 'NONE', *, *, #12507, .F. ) ;
#5508=ORIENTED_EDGE ( 'NONE', *, *, #11175, .T. ) ;
#5512=( LENGTH_UNIT ( ) NAMED_UNIT ( * ) SI_UNIT ( $, .METRE. ) );
#5519=EDGE_CURVE ( 'NONE', #796, #5799, #13624, .T. ) ;
#5521=EDGE_LOOP ( 'NONE', ( #17, #7088 ) ) ;
#5532=DIRECTION ( 'NONE',  ( 0.000000000000000000, 0.000000000000000000, -1.000000000000000000 ) ) ;
#5533=FACE_OUTER_BOUND ( 'NONE', #1506, .T. ) ;
#5534=EDGE_LOOP ( 'NONE', ( #15087, #1464, #1923, #12218, #15397, #12381 ) ) ;
#5537=CARTESIAN_POINT ( 'NONE',  ( 0.000000000000000000, 2.393700787401575436, 0.000000000000000000 ) ) ;
#5539=CARTESIAN_POINT ( 'NONE',  ( -0.7455328141524873997, 1.043307086614173151, 0.3622425942647021779 ) ) ;
#5541=DIRECTION ( 'NONE',  ( -1.000000000000000000, 0.000000000000000000, 0.000000000000000000 ) ) ;
#5546=DIRECTION ( 'NONE',  ( 0.000000000000000000, 1.000000000000000000, 0.000000000000000000 ) ) ;
#5551=EDGE_CURVE ( 'NONE', #1254, #4333, #10870, .T. ) ;
#5570=CYLINDRICAL_SURFACE ( 'NONE', #6686, 0.5511811023622046335 ) ;
#5571=EDGE_CURVE ( 'NONE', #11092, #6371, #11374, .T. ) ;
#5578=AXIS2_PLACEMENT_3D ( 'NONE', #7389, #10997, #2612 ) ;
#5580=EDGE_CURVE ( 'NONE', #692, #12461, #1875, .T. ) ;
#5590=( GEOMETRIC_REPRESENTATION_CONTEXT ( 3 ) GLOBAL_UNCERTAINTY_ASSIGNED_CONTEXT ( ( #10030 ) ) GLOBAL_UNIT_ASSIGNED_CONTEXT ( ( #12326, #9765, #4966 ) ) REPRESENTATION_CONTEXT ( 'NONE', 'WORKASPACE' ) );
#5601=AXIS2_PLACEMENT_3D ( 'NONE', #5223, #9952, #8834 ) ;
#5604=CIRCLE ( 'NONE', #15125, 0.5984251968503937480 ) ;
#5609=EDGE_CURVE ( 'NONE', #15326, #12818, #1642, .T. ) ;
#5613=CARTESIAN_POINT ( 'NONE',  ( -0.05905511811023622659, 1.338582677165354395, -0.5955041639236611228 ) ) ;
#5614=CARTESIAN_POINT ( 'NONE',  ( 7.183951695785653893E-17, 2.440944881889763884, 0.5826771653543306728 ) ) ;
#5616=EDGE_LOOP ( 'NONE', ( #10648, #5499, #7529, #1074 ) ) ;
#5619=AXIS2_PLACEMENT_3D ( 'NONE', #8183, #11862, #980 ) ;
#5620=CIRCLE ( 'NONE', #8639, 0.5511811023622046335 ) ;
#5621=ORIENTED_EDGE ( 'NONE', *, *, #5688, .T. ) ;
#5630=VECTOR ( 'NONE', #15320, 39.37007874015748143 ) ;
#5632=ORIENTED_EDGE ( 'NONE', *, *, #378, .F. ) ;
#5634=DIRECTION ( 'NONE',  ( 0.000000000000000000, -1.000000000000000000, -0.000000000000000000 ) ) ;
#5638=DIRECTION ( 'NONE',  ( -0.000000000000000000, -0.000000000000000000, -1.000000000000000000 ) ) ;
#5639=CIRCLE ( 'NONE', #7899, 0.5984251968503937480 ) ;
#5642=ORIENTED_EDGE ( 'NONE', *, *, #14749, .F. ) ;
#5644=AXIS2_PLACEMENT_3D ( 'NONE', #12328, #8889, #9118 ) ;
#5650=CARTESIAN_POINT ( 'NONE',  ( 0.1259842519685039353, 2.440944881889763884, -0.04724409448818898266 ) ) ;
#5652=AXIS2_PLACEMENT_3D ( 'NONE', #3261, #8032, #10473 ) ;
#5654=DIRECTION ( 'NONE',  ( 0.000000000000000000, 1.000000000000000000, 0.000000000000000000 ) ) ;
#5659=ADVANCED_FACE ( 'NONE', ( #2989, #5237 ), #3931, .F. ) ;
#5666=VERTEX_POINT ( 'NONE', #4072 ) ;
#5668=CARTESIAN_POINT ( 'NONE',  ( -0.1181102362204724532, 2.637795275590551825, 0.03937007874015747977 ) ) ;
#5676=CARTESIAN_POINT ( 'NONE',  ( 0.000000000000000000, 1.661417322834646049, 0.000000000000000000 ) ) ;
#5678=EDGE_LOOP ( 'NONE', ( #6503, #8981, #6160, #8472, #10741, #779 ) ) ;
#5680=AXIS2_PLACEMENT_3D ( 'NONE', #1735, #5541, #784 ) ;
#5681=ORIENTED_EDGE ( 'NONE', *, *, #636, .F. ) ;
#5682=ORIENTED_EDGE ( 'NONE', *, *, #3505, .T. ) ;
#5684=CIRCLE ( 'NONE', #15460, 0.007874015748031516770 ) ;
#5688=EDGE_CURVE ( 'NONE', #12371, #6809, #12149, .T. ) ;
#5690=FACE_OUTER_BOUND ( 'NONE', #8291, .T. ) ;
#5691=DIRECTION ( 'NONE',  ( 0.000000000000000000, 0.000000000000000000, -1.000000000000000000 ) ) ;
#5692=DIRECTION ( 'NONE',  ( 0.000000000000000000, 0.000000000000000000, 1.000000000000000000 ) ) ;
#5699=ORIENTED_EDGE ( 'NONE', *, *, #6598, .F. ) ;
#5700=VERTEX_POINT ( 'NONE', #12248 ) ;
#5703=ORIENTED_EDGE ( 'NONE', *, *, #10059, .F. ) ;
#5710=CARTESIAN_POINT ( 'NONE',  ( 0.5412721729274246885, 1.041728495490239714, 0.2430720373988119742 ) ) ;
#5722=CARTESIAN_POINT ( 'NONE',  ( 0.1181102362204724671, 2.444206406002937815, -0.03937007874015747977 ) ) ;
#5730=CARTESIAN_POINT ( 'NONE',  ( 6.846450609406462919E-17, 0.5590551181102362266, -0.5590551181102362266 ) ) ;
#5734=CARTESIAN_POINT ( 'NONE',  ( 0.05905511811023622659, 1.338582677165354395, -0.5955041639236611228 ) ) ;
#5735=VERTEX_POINT ( 'NONE', #724 ) ;
#5744=DIRECTION ( 'NONE',  ( 0.4999999999999919509, -0.000000000000000000, -0.8660254037844432595 ) ) ;
#5750=EDGE_LOOP ( 'NONE', ( #2924, #10695, #11223, #10950, #5412, #15433, #7510 ) ) ;
#5755=ORIENTED_EDGE ( 'NONE', *, *, #4043, .T. ) ;
#5769=ORIENTED_EDGE ( 'NONE', *, *, #7214, .F. ) ;
#5780=DIRECTION ( 'NONE',  ( -1.000000000000000000, -4.625929269271485914E-16, -2.309263891220325920E-14 ) ) ;
#5785=VERTEX_POINT ( 'NONE', #6893 ) ;
#5789=EDGE_LOOP ( 'NONE', ( #10728, #8349 ) ) ;
#5791=FACE_OUTER_BOUND ( 'NONE', #8136, .T. ) ;
#5792=DIRECTION ( 'NONE',  ( -0.000000000000000000, -1.000000000000000000, -0.000000000000000000 ) ) ;
#5797=CARTESIAN_POINT ( 'NONE',  ( 0.000000000000000000, 2.433070866141732846, -0.5905511811023621549 ) ) ;
#5799=VERTEX_POINT ( 'NONE', #2032 ) ;
#5803=DIRECTION ( 'NONE',  ( 1.000000000000000000, -0.000000000000000000, 1.224646799147353207E-16 ) ) ;
#5809=LINE ( 'NONE', #6623, #11122 ) ;
#5811=AXIS2_PLACEMENT_3D ( 'NONE', #13919, #7728, #1708 ) ;
#5830=VECTOR ( 'NONE', #4963, 39.37007874015748143 ) ;
#5832=EDGE_CURVE ( 'NONE', #1180, #12971, #8060, .T. ) ;
#5834=CARTESIAN_POINT ( 'NONE',  ( -0.5412478373021294420, 1.346456692913385877, 0.2362233606508100381 ) ) ;
#5837=DIRECTION ( 'NONE',  ( 0.000000000000000000, 1.000000000000000000, 0.000000000000000000 ) ) ;
#5840=DIRECTION ( 'NONE',  ( -0.000000000000000000, -1.000000000000000000, -0.000000000000000000 ) ) ;
#5841=LINE ( 'NONE', #11992, #4142 ) ;
#5842=ORIENTED_EDGE ( 'NONE', *, *, #3235, .T. ) ;
#5846=CIRCLE ( 'NONE', #3114, 0.5433070866141731514 ) ;
#5854=DIRECTION ( 'NONE',  ( -0.8660254037844431485, 4.956352788505159323E-16, -0.4999999999999918954 ) ) ;
#5859=B_SPLINE_CURVE_WITH_KNOTS ( 'NONE', 3,
 ( #6401, #11195, #3915, #3824 ),
 .UNSPECIFIED., .F., .F.,
 ( 4, 4 ),
 ( -2.828444569876537743E-06, 0.0002461255424396399509 ),
 .UNSPECIFIED. ) ;
#5867=CIRCLE ( 'NONE', #14647, 0.007874015748031516770 ) ;
#5877=CIRCLE ( 'NONE', #3405, 0.7007874015748031260 ) ;
#5883=CYLINDRICAL_SURFACE ( 'NONE', #7599, 0.007874015748031499423 ) ;
#5885=CARTESIAN_POINT ( 'NONE',  ( 0.000000000000000000, 0.3464566929133857109, -0.5590551181102362266 ) ) ;
#5886=ORIENTED_EDGE ( 'NONE', *, *, #10590, .F. ) ;
#5889=CIRCLE ( 'NONE', #158, 0.5984251968503937480 ) ;
#5890=CIRCLE ( 'NONE', #8653, 0.7086614173228346081 ) ;
#5891=LINE ( 'NONE', #4730, #8457 ) ;
#5897=EDGE_LOOP ( 'NONE', ( #4355, #6093, #8243, #13175 ) ) ;
#5904=DIRECTION ( 'NONE',  ( -1.000000000000000000, 0.000000000000000000, 0.000000000000000000 ) ) ;
#5915=ORIENTED_EDGE ( 'NONE', *, *, #5957, .F. ) ;
#5916=ORIENTED_EDGE ( 'NONE', *, *, #14623, .T. ) ;
#5917=ORIENTED_EDGE ( 'NONE', *, *, #6598, .T. ) ;
#5922=DIRECTION ( 'NONE',  ( 0.000000000000000000, 0.000000000000000000, -1.000000000000000000 ) ) ;
#5928=CYLINDRICAL_SURFACE ( 'NONE', #11188, 0.6692913385826770867 ) ;
#5932=ORIENTED_EDGE ( 'NONE', *, *, #7203, .T. ) ;
#5935=VECTOR ( 'NONE', #2407, 39.37007874015748143 ) ;
#5942=EDGE_CURVE ( 'NONE', #9581, #5785, #7245, .T. ) ;
#5952=CARTESIAN_POINT ( 'NONE',  ( -0.06692913385826772255, 0.000000000000000000, -0.5946706712680680518 ) ) ;
#5957=EDGE_CURVE ( 'NONE', #13359, #11417, #7137, .T. ) ;
#5959=CYLINDRICAL_SURFACE ( 'NONE', #4823, 0.007874015748031516770 ) ;
#5965=DIRECTION ( 'NONE',  ( -1.000000000000000000, 0.000000000000000000, 0.000000000000000000 ) ) ;
#5969=DIRECTION ( 'NONE',  ( 0.4999999999999918954, -0.000000000000000000, -0.8660254037844431485 ) ) ;
#5973=ORIENTED_EDGE ( 'NONE', *, *, #3802, .T. ) ;
#5976=DIRECTION ( 'NONE',  ( -0.000000000000000000, -1.000000000000000000, -0.000000000000000000 ) ) ;
#5977=ADVANCED_FACE ( 'NONE', ( #7031 ), #1313, .F. ) ;
#5978=CARTESIAN_POINT ( 'NONE',  ( 0.000000000000000000, 0.3070866141732283561, 0.000000000000000000 ) ) ;
#5984=DIRECTION ( 'NONE',  ( 0.000000000000000000, 1.000000000000000000, 0.000000000000000000 ) ) ;
#5998=DIRECTION ( 'NONE',  ( -1.224646799147343593E-16, 0.000000000000000000, -1.000000000000000000 ) ) ;
#6003=DIRECTION ( 'NONE',  ( 0.000000000000000000, 0.000000000000000000, -1.000000000000000000 ) ) ;
#6004=CARTESIAN_POINT ( 'NONE',  ( -0.1181102362204724532, 2.637795275590551825, -0.03937007874015747977 ) ) ;
#6005=VERTEX_POINT ( 'NONE', #4915 ) ;
#6016=CARTESIAN_POINT ( 'NONE',  ( -0.7205731843802207770, 1.190944881889763884, 0.4842140986486909715 ) ) ;
#6018=CARTESIAN_POINT ( 'NONE',  ( -0.6523822077042805700, 1.190944881889763884, 0.4448440199085330615 ) ) ;
#6028=DIRECTION ( 'NONE',  ( 1.000000000000000000, -0.000000000000000000, 1.224646799147353207E-16 ) ) ;
#6034=ADVANCED_FACE ( 'NONE', ( #3581 ), #1902, .T. ) ;
#6039=EDGE_LOOP ( 'NONE', ( #9081, #14990, #12635, #676 ) ) ;
#6040=ORIENTED_EDGE ( 'NONE', *, *, #12425, .T. ) ;
#6041=CARTESIAN_POINT ( 'NONE',  ( -0.05905511811023622659, 1.190944881889763884, -0.7874015748031497619 ) ) ;
#6042=DIRECTION ( 'NONE',  ( 0.000000000000000000, 0.000000000000000000, 1.000000000000000000 ) ) ;
#6045=CARTESIAN_POINT ( 'NONE',  ( 0.000000000000000000, 0.000000000000000000, -0.5905511811023621549 ) ) ;
#6046=CARTESIAN_POINT ( 'NONE',  ( 0.6864776960422567242, 1.338582677165354395, 0.4645290592786021633 ) ) ;
#6048=DIRECTION ( 'NONE',  ( 0.000000000000000000, 0.000000000000000000, 1.000000000000000000 ) ) ;
#6055=EDGE_CURVE ( 'NONE', #11857, #10793, #11651, .T. ) ;
#6058=EDGE_LOOP ( 'NONE', ( #4680, #2541, #8484, #12066 ) ) ;
#6061=LINE ( 'NONE', #8353, #5935 ) ;
#6066=CARTESIAN_POINT ( 'NONE',  ( 0.000000000000000000, 2.637795275590551825, 0.03937007874015747977 ) ) ;
#6072=ORIENTED_EDGE ( 'NONE', *, *, #6478, .F. ) ;
#6074=ORIENTED_EDGE ( 'NONE', *, *, #12271, .T. ) ;
#6082=PLANE ( 'NONE',  #8615 ) ;
#6084=FACE_BOUND ( 'NONE', #10662, .T. ) ;
#6093=ORIENTED_EDGE ( 'NONE', *, *, #4067, .T. ) ;
#6108=DIRECTION ( 'NONE',  ( -0.4999999999999919509, 0.000000000000000000, 0.8660254037844432595 ) ) ;
#6113=DIRECTION ( 'NONE',  ( -0.000000000000000000, -1.000000000000000000, -0.000000000000000000 ) ) ;
#6114=CARTESIAN_POINT ( 'NONE',  ( 0.000000000000000000, 0.04724409448818898960, 0.000000000000000000 ) ) ;
#6115=AXIS2_PLACEMENT_3D ( 'NONE', #6066, #14315, #14249 ) ;
#6123=EDGE_CURVE ( 'NONE', #9010, #2747, #11917, .T. ) ;
#6124=DIRECTION ( 'NONE',  ( 1.000000000000000000, 0.000000000000000000, 0.000000000000000000 ) ) ;
#6125=ADVANCED_FACE ( 'NONE', ( #9848 ), #1705, .F. ) ;
#6126=FACE_OUTER_BOUND ( 'NONE', #13479, .T. ) ;
#6130=CARTESIAN_POINT ( 'NONE',  ( 0.000000000000000000, 0.3149606299212598381, 0.000000000000000000 ) ) ;
#6141=ORIENTED_EDGE ( 'NONE', *, *, #13073, .F. ) ;
#6142=AXIS2_PLACEMENT_3D ( 'NONE', #14041, #11608, #7933 ) ;
#6144=EDGE_LOOP ( 'NONE', ( #15065, #10824, #5917, #7734, #5450, #2320 ) ) ;
#6147=EDGE_CURVE ( 'NONE', #3165, #12754, #14664, .T. ) ;
#6155=DIRECTION ( 'NONE',  ( -1.000000000000000000, -0.000000000000000000, 0.000000000000000000 ) ) ;
#6160=ORIENTED_EDGE ( 'NONE', *, *, #14986, .T. ) ;
#6168=AXIS2_PLACEMENT_3D ( 'NONE', #11343, #13475, #1558 ) ;
#6170=EDGE_CURVE ( 'NONE', #11777, #10892, #5639, .T. ) ;
#6182=DIRECTION ( 'NONE',  ( 0.000000000000000000, 1.000000000000000000, 0.000000000000000000 ) ) ;
#6183=AXIS2_PLACEMENT_3D ( 'NONE', #7722, #4115, #10001 ) ;
#6186=LINE ( 'NONE', #14670, #13862 ) ;
#6188=FACE_OUTER_BOUND ( 'NONE', #6518, .T. ) ;
#6194=FACE_OUTER_BOUND ( 'NONE', #4480, .T. ) ;
#6197=DIRECTION ( 'NONE',  ( 0.000000000000000000, 0.000000000000000000, 1.000000000000000000 ) ) ;
#6198=CIRCLE ( 'NONE', #1467, 0.1476377952755906220 ) ;
#6202=AXIS2_PLACEMENT_3D ( 'NONE', #14712, #3972, #10939 ) ;
#6210=CARTESIAN_POINT ( 'NONE',  ( -0.5484644751328247025, 0.000000000000000000, 0.2393730054594876144 ) ) ;
#6224=CARTESIAN_POINT ( 'NONE',  ( 0.000000000000000000, 0.5905511811023621549, 0.000000000000000000 ) ) ;
#6225=CARTESIAN_POINT ( 'NONE',  ( 0.000000000000000000, 0.03149606299212599769, 0.000000000000000000 ) ) ;
#6226=ADVANCED_FACE ( 'NONE', ( #11014, #8750 ), #295, .T. ) ;
#6228=DIRECTION ( 'NONE',  ( 8.673617379884028076E-17, -1.000000000000000000, 0.000000000000000000 ) ) ;
#6229=EDGE_CURVE ( 'NONE', #5785, #9354, #5889, .T. ) ;
#6233=ORIENTED_EDGE ( 'NONE', *, *, #7579, .F. ) ;
#6234=EDGE_CURVE ( 'NONE', #15326, #11438, #598, .T. ) ;
#6237=CARTESIAN_POINT ( 'NONE',  ( 0.5450083523900213223, 1.338582677165354395, 0.2464697422870268384 ) ) ;
#6239=DIRECTION ( 'NONE',  ( -0.8660254037844431485, 0.000000000000000000, -0.4999999999999918954 ) ) ;
#6245=CARTESIAN_POINT ( 'NONE',  ( -0.05905511811023622659, 1.043263280880422528, -0.5946706712680680518 ) ) ;
#6247=EDGE_LOOP ( 'NONE', ( #5682, #10991 ) ) ;
#6258=DIRECTION ( 'NONE',  ( 0.5000000000000041078, -0.000000000000000000, 0.8660254037844363761 ) ) ;
#6262=SHAPE_REPRESENTATION ( 'Housing', ( #11481 ), #7464 ) ;
#6267=DIRECTION ( 'NONE',  ( -1.000000000000000000, 0.000000000000000000, 0.000000000000000000 ) ) ;
#6274=CYLINDRICAL_SURFACE ( 'NONE', #14887, 0.5905511811023621549 ) ;
#6275=DIRECTION ( 'NONE',  ( 0.000000000000000000, 0.000000000000000000, 1.000000000000000000 ) ) ;
#6280=ORIENTED_EDGE ( 'NONE', *, *, #14890, .F. ) ;
#6282=PRODUCT_DEFINITION ( 'UNKNOWN', '', #1364, #1269 ) ;
#6288=CARTESIAN_POINT ( 'NONE',  ( 8.630384923125046426E-17, 1.377952755905512028, -0.7007874015748031260 ) ) ;
#6293=VERTEX_POINT ( 'NONE', #7880 ) ;
#6294=EDGE_LOOP ( 'NONE', ( #5769, #14344, #8085, #4586 ) ) ;
#6296=EDGE_LOOP ( 'NONE', ( #5470, #5278 ) ) ;
#6299=DIRECTION ( 'NONE',  ( 0.000000000000000000, 0.000000000000000000, 1.000000000000000000 ) ) ;
#6311=ADVANCED_FACE ( 'NONE', ( #1932 ), #6697, .T. ) ;
#6312=FACE_BOUND ( 'NONE', #5006, .T. ) ;
#6313=DIRECTION ( 'NONE',  ( 0.000000000000000000, 0.000000000000000000, 1.000000000000000000 ) ) ;
#6315=EDGE_LOOP ( 'NONE', ( #2789, #13679, #10647, #10511 ) ) ;
#6318=TOROIDAL_SURFACE ( 'NONE', #2092, 0.5826771653543306728, 0.007874015748031495954 ) ;
#6319=AXIS2_PLACEMENT_3D ( 'NONE', #4236, #5546, #11594 ) ;
#6323=B_SPLINE_CURVE_WITH_KNOTS ( 'NONE', 3,
 ( #233, #2724, #1315, #2643, #5138, #12216 ),
 .UNSPECIFIED., .F., .F.,
 ( 4, 2, 4 ),
 ( 0.000000000000000000, 0.0001791382075655866988, 0.0003582764151311733977 ),
 .UNSPECIFIED. ) ;
#6324=FACE_BOUND ( 'NONE', #14307, .T. ) ;
#6330=ORIENTED_EDGE ( 'NONE', *, *, #13619, .T. ) ;
#6333=ADVANCED_FACE ( 'NONE', ( #9822 ), #4888, .T. ) ;
#6353=CARTESIAN_POINT ( 'NONE',  ( 0.1181102362204724254, 2.440944881889764329, 0.03937007874015747977 ) ) ;
#6356=CARTESIAN_POINT ( 'NONE',  ( 0.1259842519685039353, 2.440944881889763884, 0.03937007874015747977 ) ) ;
#6360=CIRCLE ( 'NONE', #10128, 0.5984251968503937480 ) ;
#6364=CARTESIAN_POINT ( 'NONE',  ( -0.05905511811023622659, 1.043307086614173373, -0.5955041639236610118 ) ) ;
#6365=ORIENTED_EDGE ( 'NONE', *, *, #3691, .F. ) ;
#6371=VERTEX_POINT ( 'NONE', #1449 ) ;
#6382=DIRECTION ( 'NONE',  ( -0.000000000000000000, -1.000000000000000000, -0.000000000000000000 ) ) ;
#6383=DIRECTION ( 'NONE',  ( 0.000000000000000000, 0.000000000000000000, 1.000000000000000000 ) ) ;
#6389=VERTEX_POINT ( 'NONE', #2926 ) ;
#6390=ORIENTED_EDGE ( 'NONE', *, *, #5957, .T. ) ;
#6391=CIRCLE ( 'NONE', #5398, 0.1476377952755906775 ) ;
#6396=AXIS2_PLACEMENT_3D ( 'NONE', #2626, #14537, #9921 ) ;
#6401=CARTESIAN_POINT ( 'NONE',  ( -0.4751993499419962519, 1.346456692913385877, 0.3506226965216301950 ) ) ;
#6404=VERTEX_POINT ( 'NONE', #4017 ) ;
#6407=DIRECTION ( 'NONE',  ( -0.000000000000000000, -1.000000000000000000, -0.000000000000000000 ) ) ;
#6408=EDGE_LOOP ( 'NONE', ( #1924, #14657, #2462, #14473 ) ) ;
#6409=VERTEX_POINT ( 'NONE', #5180 ) ;
#6410=ADVANCED_FACE ( 'NONE', ( #11227 ), #13659, .F. ) ;
#6411=ORIENTED_EDGE ( 'NONE', *, *, #3982, .T. ) ;
#6413=EDGE_CURVE ( 'NONE', #7977, #13096, #15415, .T. ) ;
#6414=B_SPLINE_CURVE_WITH_KNOTS ( 'NONE', 3,
 ( #2738, #14738, #174, #10020, #12064, #394 ),
 .UNSPECIFIED., .F., .F.,
 ( 4, 2, 4 ),
 ( 0.000000000000000000, 0.0001791382075655877830, 0.0003582764151311755661 ),
 .UNSPECIFIED. ) ;
#6415=CARTESIAN_POINT ( 'NONE',  ( -0.7455328141524873997, 1.190944881889763884, 0.3622425942647021779 ) ) ;
#6451=EDGE_CURVE ( 'NONE', #6858, #11438, #6901, .T. ) ;
#6453=VERTEX_POINT ( 'NONE', #10046 ) ;
#6456=EDGE_CURVE ( 'NONE', #14956, #715, #14920, .T. ) ;
#6457=CIRCLE ( 'NONE', #3968, 0.007874015748031516770 ) ;
#6458=DIRECTION ( 'NONE',  ( 0.000000000000000000, 1.000000000000000000, 0.000000000000000000 ) ) ;
#6462=ADVANCED_FACE ( 'NONE', ( #8075 ), #13663, .T. ) ;
#6466=FACE_OUTER_BOUND ( 'NONE', #15039, .T. ) ;
#6468=DIRECTION ( 'NONE',  ( 0.000000000000000000, 1.000000000000000000, 0.000000000000000000 ) ) ;
#6474=EDGE_LOOP ( 'NONE', ( #468, #8610 ) ) ;
#6478=EDGE_CURVE ( 'NONE', #10823, #6490, #1411, .T. ) ;
#6479=FACE_OUTER_BOUND ( 'NONE', #12934, .T. ) ;
#6482=DIRECTION ( 'NONE',  ( 0.000000000000000000, 1.000000000000000000, 0.000000000000000000 ) ) ;
#6489=ORIENTED_EDGE ( 'NONE', *, *, #3176, .F. ) ;
#6490=VERTEX_POINT ( 'NONE', #13969 ) ;
#6498=FACE_OUTER_BOUND ( 'NONE', #1072, .T. ) ;
#6503=ORIENTED_EDGE ( 'NONE', *, *, #12210, .T. ) ;
#6504=DIRECTION ( 'NONE',  ( -0.000000000000000000, -1.000000000000000000, -0.000000000000000000 ) ) ;
#6508=CARTESIAN_POINT ( 'NONE',  ( 0.000000000000000000, 0.3070866141732283561, 0.000000000000000000 ) ) ;
#6512=FACE_OUTER_BOUND ( 'NONE', #1515, .T. ) ;
#6518=EDGE_LOOP ( 'NONE', ( #13574, #4209, #10763, #7001 ) ) ;
#6519=VERTEX_POINT ( 'NONE', #4310 ) ;
#6523=SHAPE_REPRESENTATION_RELATIONSHIP ( 'NONE' , 'NONE' ,  #6262, #15308 ) ;
#6525=CARTESIAN_POINT ( 'NONE',  ( 0.5412478373021326616, 0.000000000000000000, 0.2362233606508025163 ) ) ;
#6528=DIRECTION ( 'NONE',  ( 0.000000000000000000, 4.565061778886334044E-16, 1.000000000000000000 ) ) ;
#6533=ORIENTED_EDGE ( 'NONE', *, *, #4978, .T. ) ;
#6538=FACE_OUTER_BOUND ( 'NONE', #8325, .T. ) ;
#6544=CARTESIAN_POINT ( 'NONE',  ( -0.4751993499419963074, 0.000000000000000000, 0.3506226965216301950 ) ) ;
#6546=CARTESIAN_POINT ( 'NONE',  ( 0.05905511811023622659, 1.043292445042268257, -0.5949473527966270270 ) ) ;
#6548=DIRECTION ( 'NONE',  ( 0.000000000000000000, 0.000000000000000000, -1.000000000000000000 ) ) ;
#6554=EDGE_LOOP ( 'NONE', ( #11932, #2542, #15160, #2042 ) ) ;
#6565=DIRECTION ( 'NONE',  ( 0.000000000000000000, 0.000000000000000000, 1.000000000000000000 ) ) ;
#6566=CARTESIAN_POINT ( 'NONE',  ( 0.000000000000000000, 1.425196850393700920, 0.000000000000000000 ) ) ;
#6567=AXIS2_PLACEMENT_3D ( 'NONE', #13929, #2086, #4687 ) ;
#6573=CIRCLE ( 'NONE', #8089, 0.5905511811023621549 ) ;
#6583=AXIS2_PLACEMENT_3D ( 'NONE', #13435, #14836, #13669 ) ;
#6585=CARTESIAN_POINT ( 'NONE',  ( 0.000000000000000000, 2.440944881889763884, -0.5826771653543306728 ) ) ;
#6595=AXIS2_PLACEMENT_3D ( 'NONE', #6962, #5840, #4695 ) ;
#6598=EDGE_CURVE ( 'NONE', #7333, #5666, #970, .T. ) ;
#6616=EDGE_CURVE ( 'NONE', #5070, #12857, #3619, .T. ) ;
#6619=TOROIDAL_SURFACE ( 'NONE', #1644, 0.7007874015748031260, 0.007874015748031495954 ) ;
#6620=ADVANCED_FACE ( 'NONE', ( #3701 ), #3579, .F. ) ;
#6622=CIRCLE ( 'NONE', #8144, 0.6692913385826770867 ) ;
#6623=CARTESIAN_POINT ( 'NONE',  ( 7.232166136696967594E-17, 0.000000000000000000, 0.5905511811023621549 ) ) ;
#6624=ADVANCED_FACE ( 'NONE', ( #14274 ), #5959, .F. ) ;
#6625=CARTESIAN_POINT ( 'NONE',  ( -0.06604848736013260724, 1.346456692913385877, -0.5868460571724354313 ) ) ;
#6632=CARTESIAN_POINT ( 'NONE',  ( 0.05905511811023622659, 1.338582677165354395, -0.8267716535433070613 ) ) ;
#6635=VECTOR ( 'NONE', #4089, 39.37007874015747433 ) ;
#6639=CIRCLE ( 'NONE', #1907, 0.1653543307086614012 ) ;
#6645=CARTESIAN_POINT ( 'NONE',  ( 0.000000000000000000, 0.000000000000000000, -0.6692913385826770867 ) ) ;
#6646=EDGE_CURVE ( 'NONE', #12485, #1542, #13575, .T. ) ;
#6648=DIRECTION ( 'NONE',  ( 0.000000000000000000, 0.000000000000000000, -1.000000000000000000 ) ) ;
#6675=EDGE_LOOP ( 'NONE', ( #3923, #7007, #12519, #5023, #6533, #14553, #13923 ) ) ;
#6680=CARTESIAN_POINT ( 'NONE',  ( 0.1181102362204724532, 2.637795275590551825, -0.03937007874015747977 ) ) ;
#6682=ORIENTED_EDGE ( 'NONE', *, *, #6616, .F. ) ;
#6684=ORIENTED_EDGE ( 'NONE', *, *, #13073, .T. ) ;
#6686=AXIS2_PLACEMENT_3D ( 'NONE', #1477, #7415, #10526 ) ;
#6692=CARTESIAN_POINT ( 'NONE',  ( 0.000000000000000000, 1.606299212598425674, 0.000000000000000000 ) ) ;
#6697=CYLINDRICAL_SURFACE ( 'NONE', #12905, 0.1476377952755906775 ) ;
#6698=PLANE ( 'NONE',  #13328 ) ;
#6703=AXIS2_PLACEMENT_3D ( 'NONE', #13642, #14578, #2750 ) ;
#6709=DIRECTION ( 'NONE',  ( 0.000000000000000000, 1.000000000000000000, 0.000000000000000000 ) ) ;
#6711=DIRECTION ( 'NONE',  ( 0.000000000000000000, 1.000000000000000000, 0.000000000000000000 ) ) ;
#6713=DIRECTION ( 'NONE',  ( 0.000000000000000000, 1.000000000000000000, 0.000000000000000000 ) ) ;
#6721=EDGE_CURVE ( 'NONE', #12158, #731, #6819, .T. ) ;
#6728=CARTESIAN_POINT ( 'NONE',  ( -0.4854723491485721798, 1.043263280880422528, 0.3484785681409913738 ) ) ;
#6729=DIRECTION ( 'NONE',  ( 0.000000000000000000, 0.000000000000000000, 1.000000000000000000 ) ) ;
#6732=ADVANCED_FACE ( 'NONE', ( #5791 ), #4722, .F. ) ;
#6734=CARTESIAN_POINT ( 'NONE',  ( 0.7455328141524921737, 1.043307086614173151, 0.3622425942646917418 ) ) ;
#6739=EDGE_CURVE ( 'NONE', #1672, #9404, #582, .T. ) ;
#6753=CARTESIAN_POINT ( 'NONE',  ( -0.1213717603336464113, 2.440944881889763884, 0.04263160285333146560 ) ) ;
#6757=VERTEX_POINT ( 'NONE', #7057 ) ;
#6762=B_SPLINE_CURVE_WITH_KNOTS ( 'NONE', 3,
 ( #3251, #9280, #3317, #14139 ),
 .UNSPECIFIED., .F., .F.,
 ( 4, 4 ),
 ( 0.000000000000000000, 2.119993237936496015E-05 ),
 .UNSPECIFIED. ) ;
#6763=EDGE_CURVE ( 'NONE', #14569, #5052, #2076, .T. ) ;
#6770=CARTESIAN_POINT ( 'NONE',  ( 0.05905511811023622659, 1.338582677165354395, -0.8267716535433070613 ) ) ;
#6772=VERTEX_POINT ( 'NONE', #8927 ) ;
#6780=CARTESIAN_POINT ( 'NONE',  ( 0.000000000000000000, 1.370078740157480546, 0.000000000000000000 ) ) ;
#6783=CARTESIAN_POINT ( 'NONE',  ( 0.000000000000000000, 1.417322834645669438, 0.000000000000000000 ) ) ;
#6784=CARTESIAN_POINT ( 'NONE',  ( 0.000000000000000000, 0.000000000000000000, 0.000000000000000000 ) ) ;
#6789=EDGE_LOOP ( 'NONE', ( #3568, #12354, #9748, #8493 ) ) ;
#6792=ORIENTED_EDGE ( 'NONE', *, *, #9226, .T. ) ;
#6795=ADVANCED_FACE ( 'NONE', ( #259 ), #12095, .F. ) ;
#6796=DIRECTION ( 'NONE',  ( 0.000000000000000000, 1.000000000000000000, 0.000000000000000000 ) ) ;
#6801=ORIENTED_EDGE ( 'NONE', *, *, #3396, .F. ) ;
#6802=CARTESIAN_POINT ( 'NONE',  ( 0.5445274672588121812, 1.043263280880422528, 0.2461921031270739857 ) ) ;
#6803=FACE_BOUND ( 'NONE', #7886, .T. ) ;
#6807=DIRECTION ( 'NONE',  ( 0.000000000000000000, 0.000000000000000000, 1.000000000000000000 ) ) ;
#6809=VERTEX_POINT ( 'NONE', #1430 ) ;
#6816=CARTESIAN_POINT ( 'NONE',  ( 0.6864776960422569463, 1.190944881889763884, 0.4645290592786023298 ) ) ;
#6819=CIRCLE ( 'NONE', #7086, 0.6614173228346456046 ) ;
#6822=ORIENTED_EDGE ( 'NONE', *, *, #2835, .F. ) ;
#6830=EDGE_LOOP ( 'NONE', ( #7073, #3112, #8072, #13698 ) ) ;
#6831=DIRECTION ( 'NONE',  ( -0.4999999999999919509, 0.000000000000000000, 0.8660254037844432595 ) ) ;
#6832=AXIS2_PLACEMENT_3D ( 'NONE', #12119, #1389, #13447 ) ;
#6833=ORIENTED_EDGE ( 'NONE', *, *, #8780, .T. ) ;
#6837=CIRCLE ( 'NONE', #13341, 0.03937007874015761161 ) ;
#6851=LINE ( 'NONE', #6770, #839 ) ;
#6854=AXIS2_PLACEMENT_3D ( 'NONE', #11471, #4176, #11231 ) ;
#6855=VERTEX_POINT ( 'NONE', #6625 ) ;
#6857=VERTEX_POINT ( 'NONE', #12681 ) ;
#6858=VERTEX_POINT ( 'NONE', #4278 ) ;
#6860=CIRCLE ( 'NONE', #10370, 0.05905511811023625435 ) ;
#6865=DIRECTION ( 'NONE',  ( 4.292327424963333000E-16, 1.000000000000000000, 2.478176394252540219E-16 ) ) ;
#6871=FACE_OUTER_BOUND ( 'NONE', #5750, .T. ) ;
#6888=DIRECTION ( 'NONE',  ( -0.000000000000000000, -1.000000000000000000, -0.000000000000000000 ) ) ;
#6893=CARTESIAN_POINT ( 'NONE',  ( 0.05905511811023622659, 1.043307086614173373, -0.5955041639236610118 ) ) ;
#6894=EDGE_LOOP ( 'NONE', ( #10610, #11396, #8237, #3401 ) ) ;
#6901=CIRCLE ( 'NONE', #10909, 0.6692913385826770867 ) ;
#6902=CIRCLE ( 'NONE', #2400, 0.5511811023622046335 ) ;
#6915=DIRECTION ( 'NONE',  ( 0.000000000000000000, -1.000000000000000000, -0.000000000000000000 ) ) ;
#6917=EDGE_CURVE ( 'NONE', #12818, #9404, #1574, .T. ) ;
#6944=CIRCLE ( 'NONE', #209, 0.007874015748031449116 ) ;
#6953=FACE_OUTER_BOUND ( 'NONE', #11888, .T. ) ;
#6955=CIRCLE ( 'NONE', #7958, 0.05905511811023625435 ) ;
#6960=ORIENTED_EDGE ( 'NONE', *, *, #4615, .F. ) ;
#6962=CARTESIAN_POINT ( 'NONE',  ( 0.000000000000000000, 1.645669291338583085, 0.000000000000000000 ) ) ;
#6967=ADVANCED_FACE ( 'NONE', ( #9473 ), #15094, .T. ) ;
#6975=CARTESIAN_POINT ( 'NONE',  ( 1.928577636452524610E-17, 0.007874015748031480341, 0.1574803149606299191 ) ) ;
#6977=EDGE_LOOP ( 'NONE', ( #15307, #1633 ) ) ;
#6980=LINE ( 'NONE', #1032, #10356 ) ;
#6982=DIRECTION ( 'NONE',  ( 0.000000000000000000, 1.000000000000000000, 0.000000000000000000 ) ) ;
#6986=ORIENTED_EDGE ( 'NONE', *, *, #2313, .F. ) ;
#6987=EDGE_LOOP ( 'NONE', ( #4206, #7580, #14968, #13384 ) ) ;
#6989=CIRCLE ( 'NONE', #11200, 0.5590551181102362266 ) ;
#6996=ORIENTED_EDGE ( 'NONE', *, *, #13039, .F. ) ;
#7001=ORIENTED_EDGE ( 'NONE', *, *, #950, .F. ) ;
#7007=ORIENTED_EDGE ( 'NONE', *, *, #4754, .F. ) ;
#7011=DIRECTION ( 'NONE',  ( -0.000000000000000000, -0.000000000000000000, -1.000000000000000000 ) ) ;
#7017=DIRECTION ( 'NONE',  ( 0.000000000000000000, 0.000000000000000000, 1.000000000000000000 ) ) ;
#7022=EDGE_LOOP ( 'NONE', ( #13111, #7985, #304, #6072 ) ) ;
#7023=EDGE_CURVE ( 'NONE', #1166, #4548, #2544, .T. ) ;
#7031=FACE_OUTER_BOUND ( 'NONE', #9294, .T. ) ;
#7046=VERTEX_POINT ( 'NONE', #9701 ) ;
#7054=DIMENSIONAL_EXPONENTS ( 1.000000000000000000, 0.000000000000000000, 0.000000000000000000, 0.000000000000000000, 0.000000000000000000, 0.000000000000000000, 0.000000000000000000 ) ;
#7055=ORIENTED_EDGE ( 'NONE', *, *, #4321, .F. ) ;
#7056=ORIENTED_EDGE ( 'NONE', *, *, #7107, .F. ) ;
#7057=CARTESIAN_POINT ( 'NONE',  ( 0.05905511811023625435, 2.637795275590551825, 0.03937007874015747977 ) ) ;
#7060=FACE_OUTER_BOUND ( 'NONE', #10971, .T. ) ;
#7062=DIRECTION ( 'NONE',  ( 0.8660254037844433705, 0.000000000000000000, 0.4999999999999918954 ) ) ;
#7066=FACE_OUTER_BOUND ( 'NONE', #4193, .T. ) ;
#7067=ADVANCED_FACE ( 'NONE', ( #3572, #13285 ), #1469, .F. ) ;
#7073=ORIENTED_EDGE ( 'NONE', *, *, #15440, .T. ) ;
#7077=CARTESIAN_POINT ( 'NONE',  ( 0.000000000000000000, 0.03149606299212599769, -0.1653543307086614012 ) ) ;
#7082=LINE ( 'NONE', #11737, #13364 ) ;
#7083=B_SPLINE_CURVE_WITH_KNOTS ( 'NONE', 3,
 ( #6802, #11834, #5710, #8062, #14028, #1031 ),
 .UNSPECIFIED., .F., .F.,
 ( 4, 2, 4 ),
 ( 0.000000000000000000, 0.0001791382075655873222, 0.0003582764151311746445 ),
 .UNSPECIFIED. ) ;
#7086=AXIS2_PLACEMENT_3D ( 'NONE', #11779, #1042, #13182 ) ;
#7088=ORIENTED_EDGE ( 'NONE', *, *, #1581, .T. ) ;
#7106=CARTESIAN_POINT ( 'NONE',  ( 0.000000000000000000, 2.393700787401575436, -0.5511811023622046335 ) ) ;
#7107=EDGE_CURVE ( 'NONE', #14143, #5321, #4090, .T. ) ;
#7123=CARTESIAN_POINT ( 'NONE',  ( 0.000000000000000000, 1.661417322834646049, -0.5984251968503937480 ) ) ;
#7129=DIRECTION ( 'NONE',  ( -4.292327424963297008E-16, 1.000000000000000000, 2.478176394252599876E-16 ) ) ;
#7131=CARTESIAN_POINT ( 'NONE',  ( 0.5424655050177952242, 1.338877451511696570, 0.2450016286721640457 ) ) ;
#7132=EDGE_CURVE ( 'NONE', #11777, #10377, #3608, .T. ) ;
#7134=EDGE_LOOP ( 'NONE', ( #9468, #11139, #2043, #5681 ) ) ;
#7135=ADVANCED_FACE ( 'NONE', ( #8577 ), #226, .F. ) ;
#7137=CIRCLE ( 'NONE', #879, 0.5905511811023621549 ) ;
#7139=AXIS2_PLACEMENT_3D ( 'NONE', #12314, #13648, #10415 ) ;
#7142=DIRECTION ( 'NONE',  ( 0.000000000000000000, -1.000000000000000000, 0.000000000000000000 ) ) ;
#7146=CARTESIAN_POINT ( 'NONE',  ( -0.05905511811023622659, 1.043292445042268257, -0.5949473527966270270 ) ) ;
#7151=DIRECTION ( 'NONE',  ( 0.000000000000000000, 0.000000000000000000, -1.000000000000000000 ) ) ;
#7153=AXIS2_PLACEMENT_3D ( 'NONE', #10994, #12321, #4173 ) ;
#7160=EDGE_CURVE ( 'NONE', #11226, #115, #13353, .T. ) ;
#7161=ORIENTED_EDGE ( 'NONE', *, *, #6478, .T. ) ;
#7162=ORIENTED_EDGE ( 'NONE', *, *, #3235, .F. ) ;
#7165=EDGE_CURVE ( 'NONE', #776, #14049, #3970, .T. ) ;
#7170=AXIS2_PLACEMENT_3D ( 'NONE', #3076, #12496, #7622 ) ;
#7174=CARTESIAN_POINT ( 'NONE',  ( 0.7455328141524918406, 1.338582677165354395, 0.3622425942646915753 ) ) ;
#7175=DIRECTION ( 'NONE',  ( 0.000000000000000000, 0.000000000000000000, 1.000000000000000000 ) ) ;
#7180=EDGE_LOOP ( 'NONE', ( #10935, #3252, #7161, #2959 ) ) ;
#7184=DIRECTION ( 'NONE',  ( 0.000000000000000000, -1.000000000000000000, -0.000000000000000000 ) ) ;
#7185=CIRCLE ( 'NONE', #11222, 0.6614173228346456046 ) ;
#7186=CARTESIAN_POINT ( 'NONE',  ( -0.4815353412745217998, 1.340095897400991110, 0.3474236500605538125 ) ) ;
#7199=AXIS2_PLACEMENT_3D ( 'NONE', #3707, #13256, #12077 ) ;
#7200=VERTEX_POINT ( 'NONE', #12574 ) ;
#7201=AXIS2_PLACEMENT_3D ( 'NONE', #1282, #5092, #10819 ) ;
#7203=EDGE_CURVE ( 'NONE', #1544, #9167, #3342, .T. ) ;
#7207=CARTESIAN_POINT ( 'NONE',  ( 0.000000000000000000, 0.000000000000000000, 0.000000000000000000 ) ) ;
#7214=EDGE_CURVE ( 'NONE', #9905, #8101, #13682, .T. ) ;
#7218=ORIENTED_EDGE ( 'NONE', *, *, #15282, .F. ) ;
#7222=DIRECTION ( 'NONE',  ( -0.000000000000000000, -1.000000000000000000, 0.000000000000000000 ) ) ;
#7224=DIRECTION ( 'NONE',  ( 0.000000000000000000, 0.000000000000000000, -1.000000000000000000 ) ) ;
#7245=B_SPLINE_CURVE_WITH_KNOTS ( 'NONE', 3,
 ( #1793, #6546, #15427, #13143 ),
 .UNSPECIFIED., .F., .F.,
 ( 4, 4 ),
 ( 0.000000000000000000, 2.119993237936590205E-05 ),
 .UNSPECIFIED. ) ;
#7246=CARTESIAN_POINT ( 'NONE',  ( 0.000000000000000000, 1.385826771653543510, 0.000000000000000000 ) ) ;
#7251=DIRECTION ( 'NONE',  ( 1.000000000000000000, 0.000000000000000000, 0.000000000000000000 ) ) ;
#7267=ORIENTED_EDGE ( 'NONE', *, *, #2012, .T. ) ;
#7271=DIRECTION ( 'NONE',  ( 4.292327424963333000E-16, 1.000000000000000000, 2.478176394252540712E-16 ) ) ;
#7273=DIRECTION ( 'NONE',  ( -0.000000000000000000, -1.000000000000000000, -0.000000000000000000 ) ) ;
#7278=DIRECTION ( 'NONE',  ( 0.000000000000000000, 0.000000000000000000, -1.000000000000000000 ) ) ;
#7279=CARTESIAN_POINT ( 'NONE',  ( 0.000000000000000000, 0.3228346456692913757, -0.7086614173228346081 ) ) ;
#7282=ORIENTED_EDGE ( 'NONE', *, *, #8162, .T. ) ;
#7288=CARTESIAN_POINT ( 'NONE',  ( -0.06012940348033153637, 1.041728643793834674, -0.5902917039295723090 ) ) ;
#7292=DIRECTION ( 'NONE',  ( 0.000000000000000000, 0.000000000000000000, 1.000000000000000000 ) ) ;
#7296=DIRECTION ( 'NONE',  ( 0.000000000000000000, 0.000000000000000000, -1.000000000000000000 ) ) ;
#7297=ADVANCED_FACE ( 'NONE', ( #11165 ), #13857, .T. ) ;
#7298=CARTESIAN_POINT ( 'NONE',  ( 0.000000000000000000, 1.035433070866142113, 0.000000000000000000 ) ) ;
#7306=CARTESIAN_POINT ( 'NONE',  ( -0.7796283024904574477, 1.190944881889763884, 0.3819276336347811607 ) ) ;
#7318=TOROIDAL_SURFACE ( 'NONE', #5056, 0.5984251968503937480, 0.007874015748031495954 ) ;
#7320=AXIS2_PLACEMENT_3D ( 'NONE', #8913, #14858, #10239 ) ;
#7326=LINE ( 'NONE', #12212, #15335 ) ;
#7327=CIRCLE ( 'NONE', #4091, 0.6614173228346456046 ) ;
#7331=DIRECTION ( 'NONE',  ( -0.000000000000000000, -1.000000000000000000, -0.000000000000000000 ) ) ;
#7333=VERTEX_POINT ( 'NONE', #15078 ) ;
#7337=CARTESIAN_POINT ( 'NONE',  ( -0.4815353412745563833, 0.000000000000000000, 0.3474236500605538680 ) ) ;
#7342=CARTESIAN_POINT ( 'NONE',  ( 0.000000000000000000, 0.5433070866141731514, 0.000000000000000000 ) ) ;
#7343=CARTESIAN_POINT ( 'NONE',  ( 6.750021727583836750E-17, 0.3464566929133857109, 0.5511811023622046335 ) ) ;
#7346=ORIENTED_EDGE ( 'NONE', *, *, #5942, .F. ) ;
#7349=TOROIDAL_SURFACE ( 'NONE', #5601, 0.5433070866141731514, 0.007874015748031495954 ) ;
#7350=CIRCLE ( 'NONE', #10114, 0.5905511811023621549 ) ;
#7363=CIRCLE ( 'NONE', #9386, 0.5590551181102362266 ) ;
#7366=DIRECTION ( 'NONE',  ( -0.000000000000000000, -1.000000000000000000, -0.000000000000000000 ) ) ;
#7368=DIRECTION ( 'NONE',  ( -4.292327424963298981E-16, 1.000000000000000000, 2.478176394252600369E-16 ) ) ;
#7373=DIRECTION ( 'NONE',  ( 0.000000000000000000, 0.000000000000000000, -1.000000000000000000 ) ) ;
#7383=AXIS2_PLACEMENT_3D ( 'NONE', #480, #13614, #2884 ) ;
#7389=CARTESIAN_POINT ( 'NONE',  ( 0.000000000000000000, 0.007874015748031480341, 0.000000000000000000 ) ) ;
#7399=AXIS2_PLACEMENT_3D ( 'NONE', #7246, #14533, #6275 ) ;
#7401=LINE ( 'NONE', #13505, #184 ) ;
#7402=ORIENTED_EDGE ( 'NONE', *, *, #6229, .F. ) ;
#7407=DIRECTION ( 'NONE',  ( 0.000000000000000000, 0.000000000000000000, -1.000000000000000000 ) ) ;
#7414=CARTESIAN_POINT ( 'NONE',  ( 0.05905511811023622659, 1.338582677165354395, -0.8267716535433070613 ) ) ;
#7415=DIRECTION ( 'NONE',  ( -0.000000000000000000, -1.000000000000000000, -0.000000000000000000 ) ) ;
#7430=PLANE ( 'NONE',  #13121 ) ;
#7437=FACE_OUTER_BOUND ( 'NONE', #6296, .T. ) ;
#7438=ADVANCED_FACE ( 'NONE', ( #14063 ), #3093, .F. ) ;
#7442=EDGE_LOOP ( 'NONE', ( #7218, #10308, #15023, #13265 ) ) ;
#7443=AXIS2_PLACEMENT_3D ( 'NONE', #6114, #2595, #8719 ) ;
#7449=DIRECTION ( 'NONE',  ( -0.5000000000000039968, 0.000000000000000000, -0.8660254037844362651 ) ) ;
#7460=ORIENTED_EDGE ( 'NONE', *, *, #12303, .T. ) ;
#7461=B_SPLINE_CURVE_WITH_KNOTS ( 'NONE', 3,
 ( #11689, #2344, #14336, #10738, #4542, #15283 ),
 .UNSPECIFIED., .F., .F.,
 ( 4, 2, 4 ),
 ( -2.828444569873699336E-06, 0.0001777364543001156273, 0.0003583013531701049201 ),
 .UNSPECIFIED. ) ;
#7464=( GEOMETRIC_REPRESENTATION_CONTEXT ( 3 ) GLOBAL_UNCERTAINTY_ASSIGNED_CONTEXT ( ( #13633 ) ) GLOBAL_UNIT_ASSIGNED_CONTEXT ( ( #7788, #14849, #13684 ) ) REPRESENTATION_CONTEXT ( 'NONE', 'WORKASPACE' ) );
#7465=ORIENTED_EDGE ( 'NONE', *, *, #14916, .F. ) ;
#7469=LINE ( 'NONE', #6353, #4349 ) ;
#7472=DIRECTION ( 'NONE',  ( 0.000000000000000000, 0.000000000000000000, -1.000000000000000000 ) ) ;
#7478=ORIENTED_EDGE ( 'NONE', *, *, #513, .F. ) ;
#7483=EDGE_CURVE ( 'NONE', #14569, #13096, #4103, .T. ) ;
#7505=DIRECTION ( 'NONE',  ( -1.000000000000000000, -0.000000000000000000, 0.000000000000000000 ) ) ;
#7510=ORIENTED_EDGE ( 'NONE', *, *, #3126, .F. ) ;
#7521=DIRECTION ( 'NONE',  ( 1.000000000000000000, 0.000000000000000000, -1.224646799147353207E-16 ) ) ;
#7522=CARTESIAN_POINT ( 'NONE',  ( -0.6692913385826770867, 1.614173228346457156, 0.000000000000000000 ) ) ;
#7524=DIRECTION ( 'NONE',  ( 0.4999999999999918954, -0.000000000000000000, -0.8660254037844431485 ) ) ;
#7529=ORIENTED_EDGE ( 'NONE', *, *, #2157, .F. ) ;
#7532=CARTESIAN_POINT ( 'NONE',  ( 0.000000000000000000, 2.393700787401575436, 0.5433070866141731514 ) ) ;
#7536=DIRECTION ( 'NONE',  ( 0.000000000000000000, 0.000000000000000000, 1.000000000000000000 ) ) ;
#7548=DIRECTION ( 'NONE',  ( 1.000000000000000000, 0.000000000000000000, -1.224646799147353207E-16 ) ) ;
#7551=CARTESIAN_POINT ( 'NONE',  ( 0.000000000000000000, 2.637795275590551825, 0.03937007874015747977 ) ) ;
#7553=FACE_OUTER_BOUND ( 'NONE', #2649, .T. ) ;
#7554=FACE_OUTER_BOUND ( 'NONE', #3778, .T. ) ;
#7557=ADVANCED_FACE ( 'NONE', ( #6126 ), #8860, .F. ) ;
#7577=APPLICATION_CONTEXT ( 'automotive_design' ) ;
#7579=EDGE_CURVE ( 'NONE', #2898, #12827, #11963, .T. ) ;
#7580=ORIENTED_EDGE ( 'NONE', *, *, #12425, .F. ) ;
#7586=EDGE_CURVE ( 'NONE', #115, #7799, #1602, .T. ) ;
#7587=DIRECTION ( 'NONE',  ( -0.000000000000000000, -1.000000000000000000, -0.000000000000000000 ) ) ;
#7591=AXIS2_PLACEMENT_3D ( 'NONE', #13040, #123, #9762 ) ;
#7594=VERTEX_POINT ( 'NONE', #7306 ) ;
#7595=DIRECTION ( 'NONE',  ( 0.000000000000000000, 0.000000000000000000, -1.000000000000000000 ) ) ;
#7597=VECTOR ( 'NONE', #11835, 39.37007874015748854 ) ;
#7599=AXIS2_PLACEMENT_3D ( 'NONE', #15297, #28, #10517 ) ;
#7600=DIRECTION ( 'NONE',  ( 0.000000000000000000, 1.000000000000000000, 0.000000000000000000 ) ) ;
#7603=EDGE_CURVE ( 'NONE', #8519, #12965, #2104, .T. ) ;
#7611=AXIS2_PLACEMENT_3D ( 'NONE', #3134, #2109, #10327 ) ;
#7614=DIRECTION ( 'NONE',  ( -0.000000000000000000, -1.000000000000000000, -0.000000000000000000 ) ) ;
#7618=DIRECTION ( 'NONE',  ( 0.000000000000000000, 0.000000000000000000, 1.000000000000000000 ) ) ;
#7622=DIRECTION ( 'NONE',  ( 0.000000000000000000, 0.000000000000000000, -1.000000000000000000 ) ) ;
#7625=CIRCLE ( 'NONE', #14393, 0.7086614173228346081 ) ;
#7632=ORIENTED_EDGE ( 'NONE', *, *, #13508, .F. ) ;
#7634=VERTEX_POINT ( 'NONE', #5329 ) ;
#7645=DIRECTION ( 'NONE',  ( 0.000000000000000000, 0.000000000000000000, 1.000000000000000000 ) ) ;
#7650=PLANE ( 'NONE',  #10409 ) ;
#7657=CIRCLE ( 'NONE', #4153, 0.5511811023622046335 ) ;
#7665=DIRECTION ( 'NONE',  ( 0.000000000000000000, 0.000000000000000000, -1.000000000000000000 ) ) ;
#7668=CARTESIAN_POINT ( 'NONE',  ( 0.5068643957867006167, 1.043307086614173373, 0.2244473186741426096 ) ) ;
#7669=AXIS2_PLACEMENT_3D ( 'NONE', #7689, #3059, #14676 ) ;
#7671=ORIENTED_EDGE ( 'NONE', *, *, #13005, .T. ) ;
#7679=AXIS2_PLACEMENT_3D ( 'NONE', #11576, #15193, #9240 ) ;
#7685=LINE ( 'NONE', #13410, #1712 ) ;
#7687=CARTESIAN_POINT ( 'NONE',  ( 0.000000000000000000, 1.346456692913385877, 0.000000000000000000 ) ) ;
#7689=CARTESIAN_POINT ( 'NONE',  ( 0.000000000000000000, 0.000000000000000000, 0.000000000000000000 ) ) ;
#7690=FACE_OUTER_BOUND ( 'NONE', #4331, .T. ) ;
#7692=CIRCLE ( 'NONE', #9707, 0.007874015748031516770 ) ;
#7700=EDGE_CURVE ( 'NONE', #2187, #4456, #5327, .T. ) ;
#7703=DIRECTION ( 'NONE',  ( 0.000000000000000000, 0.000000000000000000, -1.000000000000000000 ) ) ;
#7710=CARTESIAN_POINT ( 'NONE',  ( -0.1181102362204724532, 2.637795275590551825, -0.03937007874015747977 ) ) ;
#7716=CARTESIAN_POINT ( 'NONE',  ( 0.000000000000000000, 0.04724409448818898960, 0.000000000000000000 ) ) ;
#7720=DIRECTION ( 'NONE',  ( -0.8660254037844363761, 0.000000000000000000, 0.5000000000000038858 ) ) ;
#7722=CARTESIAN_POINT ( 'NONE',  ( 0.000000000000000000, 1.346456692913385877, 0.000000000000000000 ) ) ;
#7725=CARTESIAN_POINT ( 'NONE',  ( 0.000000000000000000, 1.043307086614173596, -3.902639990948922033E-18 ) ) ;
#7728=DIRECTION ( 'NONE',  ( 0.000000000000000000, 1.000000000000000000, 0.000000000000000000 ) ) ;
#7730=ORIENTED_EDGE ( 'NONE', *, *, #7781, .T. ) ;
#7734=ORIENTED_EDGE ( 'NONE', *, *, #4754, .T. ) ;
#7742=DIRECTION ( 'NONE',  ( 0.000000000000000000, 0.000000000000000000, -1.000000000000000000 ) ) ;
#7746=EDGE_CURVE ( 'NONE', #14569, #11092, #12728, .T. ) ;
#7750=ORIENTED_EDGE ( 'NONE', *, *, #14043, .F. ) ;
#7751=DIRECTION ( 'NONE',  ( -0.000000000000000000, -1.000000000000000000, -0.000000000000000000 ) ) ;
#7755=DIRECTION ( 'NONE',  ( 0.000000000000000000, 1.000000000000000000, 0.000000000000000000 ) ) ;
#7756=ORIENTED_EDGE ( 'NONE', *, *, #2756, .T. ) ;
#7759=FACE_OUTER_BOUND ( 'NONE', #10761, .T. ) ;
#7762=CARTESIAN_POINT ( 'NONE',  ( 0.7455328141524921737, 1.190944881889763884, 0.3622425942646917418 ) ) ;
#7764=ORIENTED_EDGE ( 'NONE', *, *, #14092, .F. ) ;
#7765=ADVANCED_FACE ( 'NONE', ( #13887 ), #14625, .T. ) ;
#7775=EDGE_CURVE ( 'NONE', #13421, #15234, #12816, .T. ) ;
#7781=EDGE_CURVE ( 'NONE', #14360, #5195, #7350, .T. ) ;
#7788=( CONVERSION_BASED_UNIT ( 'INCH', #14942 ) LENGTH_UNIT ( ) NAMED_UNIT ( #7054 ) );
#7795=FACE_BOUND ( 'NONE', #5179, .T. ) ;
#7797=ORIENTED_EDGE ( 'NONE', *, *, #4978, .F. ) ;
#7799=VERTEX_POINT ( 'NONE', #4947 ) ;
#7800=ADVANCED_FACE ( 'NONE', ( #10809 ), #12075, .F. ) ;
#7809=DIRECTION ( 'NONE',  ( -0.000000000000000000, -1.000000000000000000, -0.000000000000000000 ) ) ;
#7812=CYLINDRICAL_SURFACE ( 'NONE', #13944, 0.1574803149606299191 ) ;
#7818=EDGE_LOOP ( 'NONE', ( #14976, #9696, #10013, #8385 ) ) ;
#7823=EDGE_CURVE ( 'NONE', #1544, #3165, #8400, .T. ) ;
#7825=CARTESIAN_POINT ( 'NONE',  ( 0.000000000000000000, 0.000000000000000000, 0.000000000000000000 ) ) ;
#7826=DIRECTION ( 'NONE',  ( -0.000000000000000000, -1.000000000000000000, -0.000000000000000000 ) ) ;
#7831=DIRECTION ( 'NONE',  ( -0.000000000000000000, -1.000000000000000000, -0.000000000000000000 ) ) ;
#7835=FACE_OUTER_BOUND ( 'NONE', #2852, .T. ) ;
#7839=AXIS2_PLACEMENT_3D ( 'NONE', #2618, #12194, #13503 ) ;
#7843=DIRECTION ( 'NONE',  ( 0.000000000000000000, 0.000000000000000000, 1.000000000000000000 ) ) ;
#7859=AXIS2_PLACEMENT_3D ( 'NONE', #5460, #7973, #1949 ) ;
#7867=CIRCLE ( 'NONE', #4207, 0.5826771653543306728 ) ;
#7869=DIRECTION ( 'NONE',  ( 1.000000000000000000, 8.673617379884029309E-17, -0.000000000000000000 ) ) ;
#7875=AXIS2_PLACEMENT_3D ( 'NONE', #10974, #1203, #5007 ) ;
#7880=CARTESIAN_POINT ( 'NONE',  ( 0.000000000000000000, 1.622047244094488638, -0.5511811023622046335 ) ) ;
#7882=DIRECTION ( 'NONE',  ( 0.000000000000000000, -0.000000000000000000, 1.000000000000000000 ) ) ;
#7884=ORIENTED_EDGE ( 'NONE', *, *, #7603, .F. ) ;
#7886=EDGE_LOOP ( 'NONE', ( #15137, #4767 ) ) ;
#7891=EDGE_CURVE ( 'NONE', #9354, #9753, #7082, .T. ) ;
#7895=CARTESIAN_POINT ( 'NONE',  ( 0.4787092522273704853, 1.341768146560826658, 0.3474236500605594191 ) ) ;
#7899=AXIS2_PLACEMENT_3D ( 'NONE', #6224, #2780, #13371 ) ;
#7900=LINE ( 'NONE', #6632, #8438 ) ;
#7908=ORIENTED_EDGE ( 'NONE', *, *, #9935, .F. ) ;
#7918=VERTEX_POINT ( 'NONE', #10387 ) ;
#7922=DIRECTION ( 'NONE',  ( 0.000000000000000000, 0.000000000000000000, -1.000000000000000000 ) ) ;
#7928=AXIS2_PLACEMENT_3D ( 'NONE', #3631, #2368, #7151 ) ;
#7933=DIRECTION ( 'NONE',  ( 0.000000000000000000, 0.000000000000000000, 1.000000000000000000 ) ) ;
#7936=CARTESIAN_POINT ( 'NONE',  ( 0.000000000000000000, 1.417322834645669438, -0.6614173228346456046 ) ) ;
#7942=DIRECTION ( 'NONE',  ( 1.000000000000000000, 0.000000000000000000, -0.000000000000000000 ) ) ;
#7946=FACE_OUTER_BOUND ( 'NONE', #13755, .T. ) ;
#7947=CIRCLE ( 'NONE', #12964, 0.007874015748031449116 ) ;
#7951=AXIS2_PLACEMENT_3D ( 'NONE', #8286, #5136, #9849 ) ;
#7954=CARTESIAN_POINT ( 'NONE',  ( 0.000000000000000000, 0.5905511811023621549, -0.5984251968503937480 ) ) ;
#7958=AXIS2_PLACEMENT_3D ( 'NONE', #2897, #1729, #5297 ) ;
#7959=CARTESIAN_POINT ( 'NONE',  ( 0.05905511811023622659, 1.190944881889763884, -0.8267716535433072833 ) ) ;
#7962=DIRECTION ( 'NONE',  ( 0.000000000000000000, 0.000000000000000000, 1.000000000000000000 ) ) ;
#7973=DIRECTION ( 'NONE',  ( 1.000000000000000000, 0.000000000000000000, -1.224646799147353207E-16 ) ) ;
#7974=CARTESIAN_POINT ( 'NONE',  ( 0.000000000000000000, 0.5511811023622046335, 0.6614173228346456046 ) ) ;
#7975=FACE_OUTER_BOUND ( 'NONE', #3488, .T. ) ;
#7977=VERTEX_POINT ( 'NONE', #8271 ) ;
#7979=ADVANCED_FACE ( 'NONE', ( #1157 ), #1615, .T. ) ;
#7985=ORIENTED_EDGE ( 'NONE', *, *, #5571, .T. ) ;
#7989=LINE ( 'NONE', #12769, #15122 ) ;
#7994=VERTEX_POINT ( 'NONE', #7174 ) ;
#7996=FACE_OUTER_BOUND ( 'NONE', #4489, .T. ) ;
#7997=CARTESIAN_POINT ( 'NONE',  ( -0.05905511811023622659, 1.338582677165354395, -0.5955041639236611228 ) ) ;
#8002=ADVANCED_FACE ( 'NONE', ( #9691 ), #2116, .T. ) ;
#8011=SHAPE_DEFINITION_REPRESENTATION ( #15291, #6262 ) ;
#8014=ORIENTED_EDGE ( 'NONE', *, *, #7160, .T. ) ;
#8020=CARTESIAN_POINT ( 'NONE',  ( -0.4751993499419962519, 1.035433070866141891, 0.3506226965216301950 ) ) ;
#8023=ORIENTED_EDGE ( 'NONE', *, *, #4857, .F. ) ;
#8029=DIRECTION ( 'NONE',  ( -0.000000000000000000, -1.000000000000000000, -0.000000000000000000 ) ) ;
#8032=DIRECTION ( 'NONE',  ( -0.000000000000000000, -1.000000000000000000, -0.000000000000000000 ) ) ;
#8035=ORIENTED_EDGE ( 'NONE', *, *, #5609, .T. ) ;
#8039=EDGE_CURVE ( 'NONE', #8264, #2150, #5846, .T. ) ;
#8043=CARTESIAN_POINT ( 'NONE',  ( 0.000000000000000000, 1.346456692913385877, 0.000000000000000000 ) ) ;
#8050=ORIENTED_EDGE ( 'NONE', *, *, #6229, .T. ) ;
#8051=EDGE_LOOP ( 'NONE', ( #11625, #12424, #11650, #12888 ) ) ;
#8060=LINE ( 'NONE', #11686, #3647 ) ;
#8062=CARTESIAN_POINT ( 'NONE',  ( 0.5403775172679829986, 1.038795175326499676, 0.2394877259645026013 ) ) ;
#8064=CARTESIAN_POINT ( 'NONE',  ( 0.000000000000000000, 2.637795275590551825, 0.03937007874015747977 ) ) ;
#8066=DIRECTION ( 'NONE',  ( -0.000000000000000000, -1.000000000000000000, -0.000000000000000000 ) ) ;
#8067=VERTEX_POINT ( 'NONE', #12106 ) ;
#8068=DIRECTION ( 'NONE',  ( 1.000000000000000000, 0.000000000000000000, 0.000000000000000000 ) ) ;
#8072=ORIENTED_EDGE ( 'NONE', *, *, #6123, .F. ) ;
#8075=FACE_OUTER_BOUND ( 'NONE', #7022, .T. ) ;
#8078=DIRECTION ( 'NONE',  ( -0.000000000000000000, -1.000000000000000000, -0.000000000000000000 ) ) ;
#8079=CARTESIAN_POINT ( 'NONE',  ( 0.000000000000000000, 0.000000000000000000, 0.000000000000000000 ) ) ;
#8083=CIRCLE ( 'NONE', #12596, 0.6614173228346456046 ) ;
#8085=ORIENTED_EDGE ( 'NONE', *, *, #8852, .F. ) ;
#8089=AXIS2_PLACEMENT_3D ( 'NONE', #312, #7273, #2737 ) ;
#8098=AXIS2_PLACEMENT_3D ( 'NONE', #4195, #364, #2854 ) ;
#8101=VERTEX_POINT ( 'NONE', #6680 ) ;
#8104=AXIS2_PLACEMENT_3D ( 'NONE', #3228, #5634, #14987 ) ;
#8108=PLANE ( 'NONE',  #14218 ) ;
#8113=AXIS2_PLACEMENT_3D ( 'NONE', #9266, #14044, #7224 ) ;
#8123=ORIENTED_EDGE ( 'NONE', *, *, #3126, .T. ) ;
#8132=CARTESIAN_POINT ( 'NONE',  ( -0.4854723491485721798, 1.043263280880422528, 0.3484785681409913738 ) ) ;
#8136=EDGE_LOOP ( 'NONE', ( #14842, #14955, #377, #4834 ) ) ;
#8139=AXIS2_PLACEMENT_3D ( 'NONE', #14351, #8403, #13188 ) ;
#8141=AXIS2_PLACEMENT_3D ( 'NONE', #3494, #8327, #14144 ) ;
#8144=AXIS2_PLACEMENT_3D ( 'NONE', #7342, #8462, #2498 ) ;
#8162=EDGE_CURVE ( 'NONE', #12485, #6809, #13883, .T. ) ;
#8167=ORIENTED_EDGE ( 'NONE', *, *, #2906, .T. ) ;
#8168=EDGE_LOOP ( 'NONE', ( #3338, #14906, #11865, #1765 ) ) ;
#8176=CARTESIAN_POINT ( 'NONE',  ( 0.1213717603336464113, 2.440944881889763884, -0.04263160285333145172 ) ) ;
#8181=ORIENTED_EDGE ( 'NONE', *, *, #7775, .F. ) ;
#8183=CARTESIAN_POINT ( 'NONE',  ( 0.000000000000000000, 1.606299212598425674, 0.6614173228346456046 ) ) ;
#8190=ORIENTED_EDGE ( 'NONE', *, *, #6451, .F. ) ;
#8191=CARTESIAN_POINT ( 'NONE',  ( 8.196454954923229282E-17, 0.5433070866141731514, 0.6692913385826770867 ) ) ;
#8204=DIRECTION ( 'NONE',  ( 0.000000000000000000, 0.000000000000000000, -1.000000000000000000 ) ) ;
#8208=CARTESIAN_POINT ( 'NONE',  ( 0.000000000000000000, 0.5433070866141731514, -0.6692913385826770867 ) ) ;
#8209=AXIS2_PLACEMENT_3D ( 'NONE', #6225, #6382, #12515 ) ;
#8215=B_SPLINE_CURVE_WITH_KNOTS ( 'NONE', 3,
 ( #5172, #4080, #13555, #12549 ),
 .UNSPECIFIED., .F., .F.,
 ( 4, 4 ),
 ( 0.0002461255424396399509, 0.0003583013531701036733 ),
 .UNSPECIFIED. ) ;
#8220=DIRECTION ( 'NONE',  ( -0.000000000000000000, -1.000000000000000000, -0.000000000000000000 ) ) ;
#8221=CARTESIAN_POINT ( 'NONE',  ( 8.582170482213735190E-17, 0.5826771653543306728, 0.7007874015748031260 ) ) ;
#8226=CARTESIAN_POINT ( 'NONE',  ( -0.4815353412745217998, 1.041793866378536437, 0.3474236500605538125 ) ) ;
#8227=AXIS2_PLACEMENT_3D ( 'NONE', #8859, #5236, #5163 ) ;
#8237=ORIENTED_EDGE ( 'NONE', *, *, #6739, .F. ) ;
#8241=LINE ( 'NONE', #4630, #14857 ) ;
#8243=ORIENTED_EDGE ( 'NONE', *, *, #11168, .T. ) ;
#8244=ORIENTED_EDGE ( 'NONE', *, *, #9065, .T. ) ;
#8247=DIRECTION ( 'NONE',  ( 0.000000000000000000, 0.000000000000000000, 1.000000000000000000 ) ) ;
#8252=CARTESIAN_POINT ( 'NONE',  ( 0.05905511811023622659, 1.043307086614173151, -0.8267716535433072833 ) ) ;
#8260=ORIENTED_EDGE ( 'NONE', *, *, #5282, .T. ) ;
#8264=VERTEX_POINT ( 'NONE', #15067 ) ;
#8269=CARTESIAN_POINT ( 'NONE',  ( 0.000000000000000000, 0.000000000000000000, -0.5511811023622046335 ) ) ;
#8270=DIRECTION ( 'NONE',  ( 1.000000000000000000, -0.000000000000000000, 1.224646799147353207E-16 ) ) ;
#8271=CARTESIAN_POINT ( 'NONE',  ( 2.025006518275150778E-17, 0.03937007874015749365, 0.1653543307086614012 ) ) ;
#8276=ORIENTED_EDGE ( 'NONE', *, *, #4740, .T. ) ;
#8285=ORIENTED_EDGE ( 'NONE', *, *, #1800, .T. ) ;
#8286=CARTESIAN_POINT ( 'NONE',  ( 8.100026073100603114E-17, 0.3622047244094487306, 0.6614173228346456046 ) ) ;
#8289=CARTESIAN_POINT ( 'NONE',  ( 0.6523822077042866763, 1.190944881889763884, 0.4448440199085238467 ) ) ;
#8291=EDGE_LOOP ( 'NONE', ( #12029, #8190, #1779, #2330 ) ) ;
#8297=DIRECTION ( 'NONE',  ( -1.000000000000000000, 0.000000000000000000, 0.000000000000000000 ) ) ;
#8309=ORIENTED_EDGE ( 'NONE', *, *, #3982, .F. ) ;
#8311=DIRECTION ( 'NONE',  ( 0.000000000000000000, 0.000000000000000000, -1.000000000000000000 ) ) ;
#8313=FACE_OUTER_BOUND ( 'NONE', #15075, .T. ) ;
#8324=EDGE_LOOP ( 'NONE', ( #14897, #13493 ) ) ;
#8325=EDGE_LOOP ( 'NONE', ( #3212, #12699, #9523, #15445 ) ) ;
#8326=ORIENTED_EDGE ( 'NONE', *, *, #4043, .F. ) ;
#8327=DIRECTION ( 'NONE',  ( -0.000000000000000000, -1.000000000000000000, -0.000000000000000000 ) ) ;
#8333=DIRECTION ( 'NONE',  ( -0.8660254037844363761, 0.000000000000000000, 0.5000000000000038858 ) ) ;
#8336=CARTESIAN_POINT ( 'NONE',  ( 6.846450609406462919E-17, 1.614173228346457156, -0.5590551181102362266 ) ) ;
#8341=AXIS2_PLACEMENT_3D ( 'NONE', #1535, #9936, #7645 ) ;
#8349=ORIENTED_EDGE ( 'NONE', *, *, #12271, .F. ) ;
#8351=CARTESIAN_POINT ( 'NONE',  ( -0.5511811023622046335, 0.3543307086614172485, 0.000000000000000000 ) ) ;
#8352=VECTOR ( 'NONE', #147, 39.37007874015748143 ) ;
#8353=CARTESIAN_POINT ( 'NONE',  ( 0.000000000000000000, 2.448818897637795367, -0.03937007874015747977 ) ) ;
#8369=VECTOR ( 'NONE', #7751, 39.37007874015748143 ) ;
#8377=CARTESIAN_POINT ( 'NONE',  ( -0.1259842519685039353, 2.440944881889763884, -0.04724409448818898266 ) ) ;
#8380=CIRCLE ( 'NONE', #12879, 0.5590551181102362266 ) ;
#8384=AXIS2_PLACEMENT_3D ( 'NONE', #10172, #12450, #12289 ) ;
#8385=ORIENTED_EDGE ( 'NONE', *, *, #3363, .T. ) ;
#8393=TOROIDAL_SURFACE ( 'NONE', #3136, 0.6614173228346456046, 0.007874015748031495954 ) ;
#8398=AXIS2_PLACEMENT_3D ( 'NONE', #4893, #9689, #14466 ) ;
#8400=LINE ( 'NONE', #3772, #8877 ) ;
#8402=LINE ( 'NONE', #8252, #8696 ) ;
#8403=DIRECTION ( 'NONE',  ( 0.000000000000000000, 1.000000000000000000, 0.000000000000000000 ) ) ;
#8404=EDGE_CURVE ( 'NONE', #15326, #1672, #2130, .T. ) ;
#8408=DIRECTION ( 'NONE',  ( 0.8660254037844363761, 0.000000000000000000, -0.5000000000000038858 ) ) ;
#8415=ORIENTED_EDGE ( 'NONE', *, *, #14962, .F. ) ;
#8417=ORIENTED_EDGE ( 'NONE', *, *, #8741, .F. ) ;
#8418=ORIENTED_EDGE ( 'NONE', *, *, #5019, .T. ) ;
#8425=FACE_OUTER_BOUND ( 'NONE', #4795, .T. ) ;
#8427=LINE ( 'NONE', #4673, #3822 ) ;
#8432=ORIENTED_EDGE ( 'NONE', *, *, #12766, .F. ) ;
#8436=TOROIDAL_SURFACE ( 'NONE', #4429, 0.5984251968503937480, 0.007874015748031495954 ) ;
#8438=VECTOR ( 'NONE', #2974, 39.37007874015748143 ) ;
#8440=AXIS2_PLACEMENT_3D ( 'NONE', #15260, #2013, #12822 ) ;
#8449=CARTESIAN_POINT ( 'NONE',  ( 0.05905511811023625435, 2.637795275590551825, 0.03937007874015747977 ) ) ;
#8457=VECTOR ( 'NONE', #5969, 39.37007874015748854 ) ;
#8458=PLANE ( 'NONE',  #2634 ) ;
#8462=DIRECTION ( 'NONE',  ( 0.000000000000000000, 1.000000000000000000, 0.000000000000000000 ) ) ;
#8464=DIRECTION ( 'NONE',  ( -1.000000000000000000, 0.000000000000000000, 0.000000000000000000 ) ) ;
#8472=ORIENTED_EDGE ( 'NONE', *, *, #5832, .F. ) ;
#8475=ORIENTED_EDGE ( 'NONE', *, *, #15420, .F. ) ;
#8481=DIRECTION ( 'NONE',  ( 1.224646799147353947E-16, 0.000000000000000000, -1.000000000000000000 ) ) ;
#8482=CARTESIAN_POINT ( 'NONE',  ( 6.750021727583836750E-17, 0.000000000000000000, 0.5511811023622046335 ) ) ;
#8483=ADVANCED_FACE ( 'NONE', ( #6194 ), #1510, .F. ) ;
#8484=ORIENTED_EDGE ( 'NONE', *, *, #13252, .T. ) ;
#8493=ORIENTED_EDGE ( 'NONE', *, *, #10585, .F. ) ;
#8501=DIRECTION ( 'NONE',  ( 0.5000000000000041078, -0.000000000000000000, 0.8660254037844363761 ) ) ;
#8502=CARTESIAN_POINT ( 'NONE',  ( 0.000000000000000000, 0.007874015748031480341, 0.000000000000000000 ) ) ;
#8507=ORIENTED_EDGE ( 'NONE', *, *, #2012, .F. ) ;
#8513=DIRECTION ( 'NONE',  ( -0.000000000000000000, -1.000000000000000000, -0.000000000000000000 ) ) ;
#8514=CARTESIAN_POINT ( 'NONE',  ( -0.05905511811023622659, 1.190944881889763884, -0.8267716535433072833 ) ) ;
#8515=DIRECTION ( 'NONE',  ( 0.000000000000000000, 0.000000000000000000, 1.000000000000000000 ) ) ;
#8516=DIRECTION ( 'NONE',  ( -0.000000000000000000, -1.000000000000000000, -0.000000000000000000 ) ) ;
#8519=VERTEX_POINT ( 'NONE', #13262 ) ;
#8520=ORIENTED_EDGE ( 'NONE', *, *, #13005, .F. ) ;
#8521=ORIENTED_EDGE ( 'NONE', *, *, #15255, .T. ) ;
#8526=FACE_OUTER_BOUND ( 'NONE', #15428, .T. ) ;
#8537=ADVANCED_FACE ( 'NONE', ( #14449 ), #2633, .T. ) ;
#8545=ORIENTED_EDGE ( 'NONE', *, *, #14101, .F. ) ;
#8554=ORIENTED_EDGE ( 'NONE', *, *, #6739, .T. ) ;
#8556=VERTEX_POINT ( 'NONE', #4729 ) ;
#8563=FACE_OUTER_BOUND ( 'NONE', #15292, .T. ) ;
#8567=CARTESIAN_POINT ( 'NONE',  ( 0.000000000000000000, 1.622047244094488638, 0.000000000000000000 ) ) ;
#8571=ORIENTED_EDGE ( 'NONE', *, *, #4614, .T. ) ;
#8573=TOROIDAL_SURFACE ( 'NONE', #13326, 0.5433070866141731514, 0.007874015748031495954 ) ;
#8575=TOROIDAL_SURFACE ( 'NONE', #4081, 0.5984251968503937480, 0.007874015748031495954 ) ;
#8577=FACE_OUTER_BOUND ( 'NONE', #15358, .T. ) ;
#8581=DIRECTION ( 'NONE',  ( -0.000000000000000000, -1.000000000000000000, -0.000000000000000000 ) ) ;
#8582=FACE_OUTER_BOUND ( 'NONE', #4782, .T. ) ;
#8588=AXIS2_PLACEMENT_3D ( 'NONE', #6780, #6709, #836 ) ;
#8589=ADVANCED_FACE ( 'NONE', ( #12829 ), #8393, .F. ) ;
#8595=ORIENTED_EDGE ( 'NONE', *, *, #2904, .F. ) ;
#8598=ORIENTED_EDGE ( 'NONE', *, *, #276, .T. ) ;
#8602=CIRCLE ( 'NONE', #4345, 0.7007874015748031260 ) ;
#8605=CARTESIAN_POINT ( 'NONE',  ( 0.5447670804913020692, 1.338597318737259734, 0.2463304438913534455 ) ) ;
#8610=ORIENTED_EDGE ( 'NONE', *, *, #13893, .F. ) ;
#8615=AXIS2_PLACEMENT_3D ( 'NONE', #3599, #7271, #5854 ) ;
#8617=CIRCLE ( 'NONE', #2849, 0.6692913385826770867 ) ;
#8620=VERTEX_POINT ( 'NONE', #13554 ) ;
#8630=ORIENTED_EDGE ( 'NONE', *, *, #11980, .F. ) ;
#8631=EDGE_CURVE ( 'NONE', #11432, #9431, #13896, .T. ) ;
#8632=FACE_BOUND ( 'NONE', #5789, .T. ) ;
#8636=EDGE_CURVE ( 'NONE', #5052, #7977, #2389, .T. ) ;
#8639=AXIS2_PLACEMENT_3D ( 'NONE', #11827, #535, #2792 ) ;
#8648=DIRECTION ( 'NONE',  ( 0.000000000000000000, 0.000000000000000000, 1.000000000000000000 ) ) ;
#8651=AXIS2_PLACEMENT_3D ( 'NONE', #503, #11292, #14595 ) ;
#8653=AXIS2_PLACEMENT_3D ( 'NONE', #3813, #9941, #6383 ) ;
#8656=ADVANCED_FACE ( 'NONE', ( #5533 ), #6619, .T. ) ;
#8661=PLANE ( 'NONE',  #1668 ) ;
#8671=DIRECTION ( 'NONE',  ( -0.000000000000000000, -1.000000000000000000, -0.000000000000000000 ) ) ;
#8674=CARTESIAN_POINT ( 'NONE',  ( 8.678599364036360127E-17, 1.385826771653543510, 0.7086614173228346081 ) ) ;
#8676=DIRECTION ( 'NONE',  ( 0.000000000000000000, 0.000000000000000000, -1.000000000000000000 ) ) ;
#8683=VERTEX_POINT ( 'NONE', #3277 ) ;
#8696=VECTOR ( 'NONE', #12017, 39.37007874015748143 ) ;
#8706=ORIENTED_EDGE ( 'NONE', *, *, #12026, .T. ) ;
#8708=CIRCLE ( 'NONE', #14233, 0.007874015748031516770 ) ;
#8711=CARTESIAN_POINT ( 'NONE',  ( 0.5412478373021326616, 1.346456692913385877, 0.2362233606508025163 ) ) ;
#8716=DIRECTION ( 'NONE',  ( -0.000000000000000000, -1.000000000000000000, -0.000000000000000000 ) ) ;
#8719=DIRECTION ( 'NONE',  ( 0.000000000000000000, 0.000000000000000000, -1.000000000000000000 ) ) ;
#8722=VERTEX_POINT ( 'NONE', #8226 ) ;
#8731=CARTESIAN_POINT ( 'NONE',  ( 0.000000000000000000, 0.3228346456692913757, 0.000000000000000000 ) ) ;
#8741=EDGE_CURVE ( 'NONE', #1544, #12965, #12651, .T. ) ;
#8750=FACE_OUTER_BOUND ( 'NONE', #5678, .T. ) ;
#8753=DIRECTION ( 'NONE',  ( -0.000000000000000000, -1.000000000000000000, -0.000000000000000000 ) ) ;
#8755=ORIENTED_EDGE ( 'NONE', *, *, #2432, .T. ) ;
#8758=ORIENTED_EDGE ( 'NONE', *, *, #14704, .T. ) ;
#8764=CARTESIAN_POINT ( 'NONE',  ( -0.5445274672588088505, 1.043263280880422528, 0.2461921031270815630 ) ) ;
#8766=CARTESIAN_POINT ( 'NONE',  ( 0.000000000000000000, 0.5590551181102362266, -0.5511811023622046335 ) ) ;
#8771=B_SPLINE_CURVE_WITH_KNOTS ( 'NONE', 3,
 ( #1934, #758, #12348, #4346 ),
 .UNSPECIFIED., .F., .F.,
 ( 4, 4 ),
 ( 0.000000000000000000, 0.0001112824830758653706 ),
 .UNSPECIFIED. ) ;
#8774=EDGE_LOOP ( 'NONE', ( #12117, #8897 ) ) ;
#8780=EDGE_CURVE ( 'NONE', #11283, #9168, #5877, .T. ) ;
#8791=VERTEX_POINT ( 'NONE', #7106 ) ;
#8792=ORIENTED_EDGE ( 'NONE', *, *, #14823, .T. ) ;
#8802=CIRCLE ( 'NONE', #9807, 0.03937007874015761161 ) ;
#8803=CARTESIAN_POINT ( 'NONE',  ( 0.000000000000000000, 0.3149606299212598381, 0.000000000000000000 ) ) ;
#8804=ORIENTED_EDGE ( 'NONE', *, *, #13389, .T. ) ;
#8806=ORIENTED_EDGE ( 'NONE', *, *, #14299, .T. ) ;
#8820=EDGE_CURVE ( 'NONE', #14360, #6809, #5841, .T. ) ;
#8826=VERTEX_POINT ( 'NONE', #8289 ) ;
#8833=TOROIDAL_SURFACE ( 'NONE', #7320, 0.6614173228346456046, 0.007874015748031495954 ) ;
#8834=DIRECTION ( 'NONE',  ( 0.000000000000000000, 0.000000000000000000, -1.000000000000000000 ) ) ;
#8835=DIRECTION ( 'NONE',  ( 0.000000000000000000, 0.000000000000000000, -1.000000000000000000 ) ) ;
#8838=LINE ( 'NONE', #10315, #12736 ) ;
#8839=B_SPLINE_CURVE_WITH_KNOTS ( 'NONE', 3,
 ( #15018, #5132, #10002, #4117 ),
 .UNSPECIFIED., .F., .F.,
 ( 4, 4 ),
 ( 0.0001112824830758653706, 0.0003582764151311737771 ),
 .UNSPECIFIED. ) ;
#8850=AXIS2_PLACEMENT_3D ( 'NONE', #10158, #2861, #3975 ) ;
#8851=AXIS2_PLACEMENT_3D ( 'NONE', #5952, #2209, #1034 ) ;
#8852=EDGE_CURVE ( 'NONE', #2525, #851, #1251, .T. ) ;
#8853=AXIS2_PLACEMENT_3D ( 'NONE', #11364, #2036, #8958 ) ;
#8854=EDGE_CURVE ( 'NONE', #11475, #6409, #5890, .T. ) ;
#8857=CARTESIAN_POINT ( 'NONE',  ( 7.135737254874341425E-17, 0.007874015748031480341, -0.5826771653543306728 ) ) ;
#8859=CARTESIAN_POINT ( 'NONE',  ( -0.4815353412745563833, 0.000000000000000000, 0.3552976658085854056 ) ) ;
#8860=TOROIDAL_SURFACE ( 'NONE', #597, 0.5984251968503937480, 0.007874015748031495954 ) ;
#8862=ORIENTED_EDGE ( 'NONE', *, *, #7214, .T. ) ;
#8865=AXIS2_PLACEMENT_3D ( 'NONE', #8064, #9873, #3920 ) ;
#8867=AXIS2_PLACEMENT_3D ( 'NONE', #12642, #5495, #15062 ) ;
#8868=CARTESIAN_POINT ( 'NONE',  ( 0.4751993499420013034, 0.000000000000000000, 0.3506226965216235336 ) ) ;
#8873=EDGE_CURVE ( 'NONE', #2210, #1254, #6902, .T. ) ;
#8877=VECTOR ( 'NONE', #13316, 39.37007874015748143 ) ;
#8879=VECTOR ( 'NONE', #13233, 39.37007874015748143 ) ;
#8883=EDGE_CURVE ( 'NONE', #12332, #450, #1266, .T. ) ;
#8889=DIRECTION ( 'NONE',  ( 0.5000000000000041078, -0.000000000000000000, 0.8660254037844363761 ) ) ;
#8892=AXIS2_PLACEMENT_3D ( 'NONE', #5012, #13026, #7062 ) ;
#8895=CARTESIAN_POINT ( 'NONE',  ( 0.4857119623810668974, 1.338597318737259734, 0.3486169089052639780 ) ) ;
#8897=ORIENTED_EDGE ( 'NONE', *, *, #11703, .T. ) ;
#8900=ORIENTED_EDGE ( 'NONE', *, *, #11027, .F. ) ;
#8905=CARTESIAN_POINT ( 'NONE',  ( 0.6864776960422569463, 1.043307086614173151, 0.4645290592786023298 ) ) ;
#8910=DIRECTION ( 'NONE',  ( -0.000000000000000000, -1.000000000000000000, -0.000000000000000000 ) ) ;
#8911=CARTESIAN_POINT ( 'NONE',  ( 8.196454954923229282E-17, 0.000000000000000000, 0.6692913385826770867 ) ) ;
#8913=CARTESIAN_POINT ( 'NONE',  ( 0.000000000000000000, 1.425196850393700920, 0.000000000000000000 ) ) ;
#8919=ORIENTED_EDGE ( 'NONE', *, *, #14101, .T. ) ;
#8920=ORIENTED_EDGE ( 'NONE', *, *, #10654, .F. ) ;
#8927=CARTESIAN_POINT ( 'NONE',  ( 7.232166136696967594E-17, 0.007874015748031480341, 0.5905511811023621549 ) ) ;
#8932=CARTESIAN_POINT ( 'NONE',  ( 0.4815353412745266848, 1.340095897400991554, 0.3474236500605469291 ) ) ;
#8933=DIRECTION ( 'NONE',  ( 0.000000000000000000, 0.000000000000000000, 1.000000000000000000 ) ) ;
#8934=DIRECTION ( 'NONE',  ( 0.000000000000000000, 0.000000000000000000, -1.000000000000000000 ) ) ;
#8940=CARTESIAN_POINT ( 'NONE',  ( -0.5447670804912987386, 1.338597318737259734, 0.2463304438913610506 ) ) ;
#8948=EDGE_CURVE ( 'NONE', #12754, #3165, #9914, .T. ) ;
#8957=ADVANCED_FACE ( 'NONE', ( #13458 ), #2725, .F. ) ;
#8958=DIRECTION ( 'NONE',  ( -1.000000000000000000, 4.625929269271485914E-16, 0.000000000000000000 ) ) ;
#8964=VECTOR ( 'NONE', #4198, 39.37007874015748143 ) ;
#8966=CARTESIAN_POINT ( 'NONE',  ( 0.5445274672588121812, 1.190944881889763884, 0.2461921031270739857 ) ) ;
#8971=FACE_OUTER_BOUND ( 'NONE', #3087, .T. ) ;
#8976=EDGE_CURVE ( 'NONE', #13096, #7977, #12916, .T. ) ;
#8978=CIRCLE ( 'NONE', #6703, 0.5905511811023621549 ) ;
#8979=CARTESIAN_POINT ( 'NONE',  ( 0.4751993499420012479, 1.035433070866141891, 0.3506226965216235336 ) ) ;
#8981=ORIENTED_EDGE ( 'NONE', *, *, #14043, .T. ) ;
#8985=CARTESIAN_POINT ( 'NONE',  ( 0.1181102362204724254, 2.440944881889764329, -0.03937007874015747977 ) ) ;
#8987=DIRECTION ( 'NONE',  ( 0.000000000000000000, 0.000000000000000000, 1.000000000000000000 ) ) ;
#8997=VERTEX_POINT ( 'NONE', #13593 ) ;
#8998=( BOUNDED_CURVE ( )  B_SPLINE_CURVE ( 3, ( #14348, #5722, #8176, #5650 ),
 .UNSPECIFIED., .F., .T. ) 
 B_SPLINE_CURVE_WITH_KNOTS ( ( 4, 4 ),
 ( 0.000000000000000000, 1.570796326794894560 ),
 .UNSPECIFIED. ) 
 CURVE ( )  GEOMETRIC_REPRESENTATION_ITEM ( )  RATIONAL_B_SPLINE_CURVE ( ( 1.000000000000000000, 0.8047378541243654926, 0.8047378541243654926, 1.000000000000000000 ) ) 
 REPRESENTATION_ITEM ( '' )  );
#9003=DIRECTION ( 'NONE',  ( -1.000000000000000000, 4.565061778886334044E-16, 0.000000000000000000 ) ) ;
#9004=DIRECTION ( 'NONE',  ( 0.000000000000000000, 1.000000000000000000, 0.000000000000000000 ) ) ;
#9005=CARTESIAN_POINT ( 'NONE',  ( 0.000000000000000000, 1.645669291338583085, 0.000000000000000000 ) ) ;
#9006=CARTESIAN_POINT ( 'NONE',  ( 8.630384923125046426E-17, 1.653543307086614567, 0.7007874015748031260 ) ) ;
#9010=VERTEX_POINT ( 'NONE', #10008 ) ;
#9011=DIRECTION ( 'NONE',  ( 1.000000000000000000, 0.000000000000000000, 0.000000000000000000 ) ) ;
#9020=DIRECTION ( 'NONE',  ( 0.000000000000000000, 1.000000000000000000, 0.000000000000000000 ) ) ;
#9022=EDGE_LOOP ( 'NONE', ( #3815, #5842, #656, #10275 ) ) ;
#9023=CARTESIAN_POINT ( 'NONE',  ( 0.000000000000000000, 1.614173228346457156, 0.000000000000000000 ) ) ;
#9024=CARTESIAN_POINT ( 'NONE',  ( -0.4854723491485721798, 1.338626482899105241, 0.3484785681409913738 ) ) ;
#9027=ORIENTED_EDGE ( 'NONE', *, *, #12522, .F. ) ;
#9029=EDGE_CURVE ( 'NONE', #856, #14427, #1041, .T. ) ;
#9031=ORIENTED_EDGE ( 'NONE', *, *, #9797, .F. ) ;
#9033=EDGE_CURVE ( 'NONE', #2747, #15395, #12056, .T. ) ;
#9034=CARTESIAN_POINT ( 'NONE',  ( 0.05905511811023622659, 1.190944881889763884, -0.7874015748031497619 ) ) ;
#9042=DIRECTION ( 'NONE',  ( 0.000000000000000000, 1.000000000000000000, 0.000000000000000000 ) ) ;
#9044=B_SPLINE_CURVE_WITH_KNOTS ( 'NONE', 3,
 ( #2361, #4725, #7146, #4557 ),
 .UNSPECIFIED., .F., .F.,
 ( 4, 4 ),
 ( 0.000000000000000000, 2.119993237936590205E-05 ),
 .UNSPECIFIED. ) ;
#9054=CARTESIAN_POINT ( 'NONE',  ( 7.328595018519593763E-17, 0.5984251968503937480, 0.5984251968503937480 ) ) ;
#9062=ORIENTED_EDGE ( 'NONE', *, *, #11927, .F. ) ;
#9065=EDGE_CURVE ( 'NONE', #2195, #10501, #12414, .T. ) ;
#9067=CARTESIAN_POINT ( 'NONE',  ( 0.7455328141524918406, 1.338582677165354395, 0.3622425942646915753 ) ) ;
#9071=ADVANCED_FACE ( 'NONE', ( #528, #759 ), #7650, .F. ) ;
#9073=FACE_OUTER_BOUND ( 'NONE', #12784, .T. ) ;
#9081=ORIENTED_EDGE ( 'NONE', *, *, #9306, .F. ) ;
#9087=FACE_OUTER_BOUND ( 'NONE', #2730, .T. ) ;
#9093=CARTESIAN_POINT ( 'NONE',  ( 0.000000000000000000, 0.3228346456692913757, 0.7007874015748031260 ) ) ;
#9094=CIRCLE ( 'NONE', #8341, 0.5433070866141731514 ) ;
#9095=CARTESIAN_POINT ( 'NONE',  ( 0.05905511811023622659, 1.190944881889763884, -0.7874015748031497619 ) ) ;
#9097=ORIENTED_EDGE ( 'NONE', *, *, #7823, .F. ) ;
#9117=ORIENTED_EDGE ( 'NONE', *, *, #13508, .T. ) ;
#9118=DIRECTION ( 'NONE',  ( 0.8660254037844363761, 0.000000000000000000, -0.5000000000000038858 ) ) ;
#9121=EDGE_CURVE ( 'NONE', #12971, #12485, #14163, .T. ) ;
#9127=ORIENTED_EDGE ( 'NONE', *, *, #11927, .T. ) ;
#9129=DIRECTION ( 'NONE',  ( 0.000000000000000000, 1.000000000000000000, 0.000000000000000000 ) ) ;
#9140=DIRECTION ( 'NONE',  ( -0.000000000000000000, -1.000000000000000000, -0.000000000000000000 ) ) ;
#9142=DIRECTION ( 'NONE',  ( 0.000000000000000000, 0.000000000000000000, 1.000000000000000000 ) ) ;
#9153=DIRECTION ( 'NONE',  ( 0.5000000000000041078, -0.000000000000000000, 0.8660254037844363761 ) ) ;
#9155=DIRECTION ( 'NONE',  ( -1.000000000000000000, 0.000000000000000000, 0.000000000000000000 ) ) ;
#9157=DIRECTION ( 'NONE',  ( -0.000000000000000000, -1.000000000000000000, -0.000000000000000000 ) ) ;
#9162=CARTESIAN_POINT ( 'NONE',  ( 7.232166136696967594E-17, 1.661417322834646049, 0.5905511811023621549 ) ) ;
#9167=VERTEX_POINT ( 'NONE', #8208 ) ;
#9168=VERTEX_POINT ( 'NONE', #4749 ) ;
#9170=ORIENTED_EDGE ( 'NONE', *, *, #8948, .T. ) ;
#9172=PLANE ( 'NONE',  #14644 ) ;
#9174=DIRECTION ( 'NONE',  ( 0.000000000000000000, 0.000000000000000000, 1.000000000000000000 ) ) ;
#9203=CARTESIAN_POINT ( 'NONE',  ( 0.000000000000000000, 0.5826771653543306728, 0.000000000000000000 ) ) ;
#9206=ORIENTED_EDGE ( 'NONE', *, *, #8948, .F. ) ;
#9213=ADVANCED_FACE ( 'NONE', ( #14305 ), #13997, .F. ) ;
#9215=DIRECTION ( 'NONE',  ( -0.5000000000000039968, 0.000000000000000000, -0.8660254037844362651 ) ) ;
#9216=AXIS2_PLACEMENT_3D ( 'NONE', #1736, #7366, #10981 ) ;
#9217=DIRECTION ( 'NONE',  ( -0.8660254037844432595, 0.000000000000000000, -0.4999999999999918954 ) ) ;
#9223=ORIENTED_EDGE ( 'NONE', *, *, #2756, .F. ) ;
#9226=EDGE_CURVE ( 'NONE', #13359, #6772, #7401, .T. ) ;
#9240=DIRECTION ( 'NONE',  ( 0.000000000000000000, 0.000000000000000000, 1.000000000000000000 ) ) ;
#9243=ADVANCED_FACE ( 'NONE', ( #12196, #219 ), #8661, .F. ) ;
#9259=CYLINDRICAL_SURFACE ( 'NONE', #12208, 0.007874015748031499423 ) ;
#9262=ORIENTED_EDGE ( 'NONE', *, *, #252, .T. ) ;
#9266=CARTESIAN_POINT ( 'NONE',  ( 0.000000000000000000, 0.03149606299212599769, 0.000000000000000000 ) ) ;
#9273=EDGE_CURVE ( 'NONE', #715, #4548, #666, .T. ) ;
#9276=CARTESIAN_POINT ( 'NONE',  ( 0.4815353412745266848, 1.041793866378536437, 0.3474236500605469291 ) ) ;
#9280=CARTESIAN_POINT ( 'NONE',  ( 0.5450083523900213223, 1.043307086614173373, 0.2464697422870267274 ) ) ;
#9282=ORIENTED_EDGE ( 'NONE', *, *, #7775, .T. ) ;
#9288=FACE_OUTER_BOUND ( 'NONE', #9802, .T. ) ;
#9291=DIRECTION ( 'NONE',  ( -0.000000000000000000, -1.000000000000000000, -0.000000000000000000 ) ) ;
#9294=EDGE_LOOP ( 'NONE', ( #3803, #13489, #2558, #12553 ) ) ;
#9306=EDGE_CURVE ( 'NONE', #5700, #2543, #999, .T. ) ;
#9310=CARTESIAN_POINT ( 'NONE',  ( 0.000000000000000000, 0.3149606299212598381, 0.000000000000000000 ) ) ;
#9312=ADVANCED_FACE ( 'NONE', ( #12330 ), #13439, .F. ) ;
#9315=FACE_BOUND ( 'NONE', #1384, .T. ) ;
#9320=DIRECTION ( 'NONE',  ( 0.000000000000000000, 0.000000000000000000, 1.000000000000000000 ) ) ;
#9322=EDGE_CURVE ( 'NONE', #8997, #5195, #15176, .T. ) ;
#9325=CARTESIAN_POINT ( 'NONE',  ( -0.4751993499419962519, 1.035433070866141891, 0.3506226965216301950 ) ) ;
#9328=EDGE_CURVE ( 'NONE', #14956, #1166, #11161, .T. ) ;
#9332=CIRCLE ( 'NONE', #10582, 0.5511811023622046335 ) ;
#9341=DIRECTION ( 'NONE',  ( 0.000000000000000000, 0.000000000000000000, -1.000000000000000000 ) ) ;
#9346=DIRECTION ( 'NONE',  ( 0.000000000000000000, 0.000000000000000000, 1.000000000000000000 ) ) ;
#9347=CIRCLE ( 'NONE', #11085, 0.5905511811023621549 ) ;
#9348=VECTOR ( 'NONE', #2973, 39.37007874015748143 ) ;
#9354=VERTEX_POINT ( 'NONE', #6364 ) ;
#9355=B_SPLINE_CURVE_WITH_KNOTS ( 'NONE', 3,
 ( #2978, #10024, #8940, #5468 ),
 .UNSPECIFIED., .F., .F.,
 ( 4, 4 ),
 ( 0.000000000000000000, 2.119993237936343888E-05 ),
 .UNSPECIFIED. ) ;
#9357=VECTOR ( 'NONE', #1696, 39.37007874015748854 ) ;
#9358=VERTEX_POINT ( 'NONE', #15069 ) ;
#9361=EDGE_CURVE ( 'NONE', #9837, #450, #3279, .T. ) ;
#9370=DIRECTION ( 'NONE',  ( 0.000000000000000000, -4.956352788505160310E-16, -1.000000000000000000 ) ) ;
#9379=VERTEX_POINT ( 'NONE', #8979 ) ;
#9383=AXIS2_PLACEMENT_3D ( 'NONE', #5885, #5965, #7292 ) ;
#9386=AXIS2_PLACEMENT_3D ( 'NONE', #95, #1337, #11938 ) ;
#9401=ORIENTED_EDGE ( 'NONE', *, *, #10840, .F. ) ;
#9404=VERTEX_POINT ( 'NONE', #4325 ) ;
#9406=FACE_OUTER_BOUND ( 'NONE', #13049, .T. ) ;
#9412=DIRECTION ( 'NONE',  ( 0.000000000000000000, 1.000000000000000000, 0.000000000000000000 ) ) ;
#9426=ADVANCED_FACE ( 'NONE', ( #7946 ), #3671, .F. ) ;
#9428=AXIS2_PLACEMENT_3D ( 'NONE', #4413, #2291, #195 ) ;
#9431=VERTEX_POINT ( 'NONE', #10057 ) ;
#9436=DIRECTION ( 'NONE',  ( -0.4999999999999919509, 0.000000000000000000, 0.8660254037844432595 ) ) ;
#9443=CARTESIAN_POINT ( 'NONE',  ( 0.6864776960422569463, 1.190944881889763884, 0.4645290592786023298 ) ) ;
#9461=CYLINDRICAL_SURFACE ( 'NONE', #2896, 0.007874015748031516770 ) ;
#9468=ORIENTED_EDGE ( 'NONE', *, *, #3363, .F. ) ;
#9469=ORIENTED_EDGE ( 'NONE', *, *, #14593, .T. ) ;
#9471=ORIENTED_EDGE ( 'NONE', *, *, #10874, .F. ) ;
#9472=TOROIDAL_SURFACE ( 'NONE', #6183, 0.5984251968503937480, 0.007874015748031495954 ) ;
#9473=FACE_OUTER_BOUND ( 'NONE', #14079, .T. ) ;
#9477=DIRECTION ( 'NONE',  ( 0.000000000000000000, 0.000000000000000000, -1.000000000000000000 ) ) ;
#9489=DIRECTION ( 'NONE',  ( 0.000000000000000000, -0.000000000000000000, 1.000000000000000000 ) ) ;
#9492=DIRECTION ( 'NONE',  ( 1.000000000000000000, -0.000000000000000000, 1.224646799147353207E-16 ) ) ;
#9493=CARTESIAN_POINT ( 'NONE',  ( 0.000000000000000000, 2.637795275590551825, -0.03937007874015747977 ) ) ;
#9517=EDGE_CURVE ( 'NONE', #288, #8683, #419, .T. ) ;
#9523=ORIENTED_EDGE ( 'NONE', *, *, #7700, .F. ) ;
#9524=EDGE_LOOP ( 'NONE', ( #12334, #13335, #2846, #5294 ) ) ;
#9532=DIRECTION ( 'NONE',  ( -0.000000000000000000, -0.000000000000000000, 1.000000000000000000 ) ) ;
#9546=ORIENTED_EDGE ( 'NONE', *, *, #10865, .T. ) ;
#9550=EDGE_LOOP ( 'NONE', ( #5489, #12521, #9546, #2816 ) ) ;
#9551=EDGE_CURVE ( 'NONE', #2150, #8264, #3911, .T. ) ;
#9558=CARTESIAN_POINT ( 'NONE',  ( -0.5403775172679798899, 1.038795175326500120, 0.2394877259645100398 ) ) ;
#9560=DIRECTION ( 'NONE',  ( -0.5000000000000039968, 0.000000000000000000, -0.8660254037844362651 ) ) ;
#9568=CARTESIAN_POINT ( 'NONE',  ( -0.7114373258145173518, 1.190944881889763884, 0.3425575548946232507 ) ) ;
#9577=CARTESIAN_POINT ( 'NONE',  ( -0.7455328141524873997, 1.190944881889763884, 0.3622425942647021779 ) ) ;
#9578=CARTESIAN_POINT ( 'NONE',  ( 8.678599364036360127E-17, 0.000000000000000000, 0.7086614173228346081 ) ) ;
#9581=VERTEX_POINT ( 'NONE', #15388 ) ;
#9582=ORIENTED_EDGE ( 'NONE', *, *, #12614, .F. ) ;
#9591=LINE ( 'NONE', #45, #12345 ) ;
#9600=CARTESIAN_POINT ( 'NONE',  ( 0.000000000000000000, 1.653543307086614567, -0.7007874015748031260 ) ) ;
#9607=TOROIDAL_SURFACE ( 'NONE', #6583, 0.7007874015748031260, 0.007874015748031495954 ) ;
#9612=DIRECTION ( 'NONE',  ( 0.000000000000000000, 0.000000000000000000, -1.000000000000000000 ) ) ;
#9615=CIRCLE ( 'NONE', #11610, 0.7086614173228346081 ) ;
#9616=AXIS2_PLACEMENT_3D ( 'NONE', #5668, #7869, #2163 ) ;
#9618=MECHANICAL_DESIGN_GEOMETRIC_PRESENTATION_REPRESENTATION('',(#1360),#5590);
#9619=EDGE_CURVE ( 'NONE', #7799, #115, #4422, .T. ) ;
#9627=DIRECTION ( 'NONE',  ( -0.000000000000000000, -1.000000000000000000, -0.000000000000000000 ) ) ;
#9636=ORIENTED_EDGE ( 'NONE', *, *, #5467, .T. ) ;
#9642=EDGE_CURVE ( 'NONE', #15219, #6857, #11944, .T. ) ;
#9643=CARTESIAN_POINT ( 'NONE',  ( -0.5405850968742077489, 1.037100910086446559, 0.2377418676363894090 ) ) ;
#9647=FACE_OUTER_BOUND ( 'NONE', #6039, .T. ) ;
#9656=ADVANCED_FACE ( 'NONE', ( #10989 ), #13187, .F. ) ;
#9662=CARTESIAN_POINT ( 'NONE',  ( 0.000000000000000000, 1.346456692913385877, 0.000000000000000000 ) ) ;
#9664=CARTESIAN_POINT ( 'NONE',  ( 0.000000000000000000, 0.000000000000000000, 0.000000000000000000 ) ) ;
#9668=LINE ( 'NONE', #8482, #863 ) ;
#9673=AXIS2_PLACEMENT_3D ( 'NONE', #10162, #11974, #1070 ) ;
#9685=DIRECTION ( 'NONE',  ( -0.000000000000000000, -1.000000000000000000, -0.000000000000000000 ) ) ;
#9689=DIRECTION ( 'NONE',  ( -0.000000000000000000, -1.000000000000000000, -0.000000000000000000 ) ) ;
#9691=FACE_OUTER_BOUND ( 'NONE', #7134, .T. ) ;
#9696=ORIENTED_EDGE ( 'NONE', *, *, #151, .T. ) ;
#9701=CARTESIAN_POINT ( 'NONE',  ( 7.232166136696967594E-17, 0.5984251968503937480, 0.5905511811023621549 ) ) ;
#9707=AXIS2_PLACEMENT_3D ( 'NONE', #5730, #3547, #1052 ) ;
#9711=DIRECTION ( 'NONE',  ( 0.000000000000000000, 0.000000000000000000, -1.000000000000000000 ) ) ;
#9721=AXIS2_PLACEMENT_3D ( 'NONE', #13079, #10890, #10739 ) ;
#9724=CARTESIAN_POINT ( 'NONE',  ( 0.000000000000000000, 0.5984251968503937480, 0.000000000000000000 ) ) ;
#9747=CARTESIAN_POINT ( 'NONE',  ( -0.05905511811023622659, 1.338626482899105241, -0.5946706712680680518 ) ) ;
#9748=ORIENTED_EDGE ( 'NONE', *, *, #12282, .F. ) ;
#9752=DIRECTION ( 'NONE',  ( 0.000000000000000000, 4.956352788505160310E-16, 1.000000000000000000 ) ) ;
#9753=VERTEX_POINT ( 'NONE', #10126 ) ;
#9756=EDGE_CURVE ( 'NONE', #5246, #9837, #10929, .T. ) ;
#9758=ORIENTED_EDGE ( 'NONE', *, *, #7579, .T. ) ;
#9762=DIRECTION ( 'NONE',  ( 0.000000000000000000, 0.000000000000000000, -1.000000000000000000 ) ) ;
#9765=( NAMED_UNIT ( * ) PLANE_ANGLE_UNIT ( ) SI_UNIT ( $, .RADIAN. ) );
#9766=DIRECTION ( 'NONE',  ( 0.000000000000000000, 0.000000000000000000, -1.000000000000000000 ) ) ;
#9767=LINE ( 'NONE', #5032, #4388 ) ;
#9768=DIRECTION ( 'NONE',  ( 0.000000000000000000, 0.000000000000000000, 1.000000000000000000 ) ) ;
#9775=CARTESIAN_POINT ( 'NONE',  ( 8.196454954923229282E-17, 1.606299212598425674, 0.6692913385826770867 ) ) ;
#9778=CARTESIAN_POINT ( 'NONE',  ( 0.000000000000000000, 0.000000000000000000, -0.7086614173228346081 ) ) ;
#9780=LINE ( 'NONE', #3672, #11841 ) ;
#9781=DIRECTION ( 'NONE',  ( -0.8660254037844433705, 0.000000000000000000, -0.4999999999999918954 ) ) ;
#9782=ORIENTED_EDGE ( 'NONE', *, *, #5942, .T. ) ;
#9783=ORIENTED_EDGE ( 'NONE', *, *, #11703, .F. ) ;
#9790=CARTESIAN_POINT ( 'NONE',  ( 0.5445274672588121812, 1.338626482899105241, 0.2461921031270739857 ) ) ;
#9797=EDGE_CURVE ( 'NONE', #9010, #8101, #12941, .T. ) ;
#9798=CARTESIAN_POINT ( 'NONE',  ( -0.5068643957866975081, 1.043307086614173373, 0.2244473186741497150 ) ) ;
#9800=ORIENTED_EDGE ( 'NONE', *, *, #14792, .F. ) ;
#9802=EDGE_LOOP ( 'NONE', ( #8630, #13258, #8862, #9031 ) ) ;
#9805=DIRECTION ( 'NONE',  ( 0.000000000000000000, 1.000000000000000000, 0.000000000000000000 ) ) ;
#9807=AXIS2_PLACEMENT_3D ( 'NONE', #2154, #6831, #12740 ) ;
#9808=DIRECTION ( 'NONE',  ( -8.881784197001253901E-15, 0.000000000000000000, -1.000000000000000000 ) ) ;
#9810=DIRECTION ( 'NONE',  ( -1.224646799147352961E-16, 0.000000000000000000, -1.000000000000000000 ) ) ;
#9811=DIRECTION ( 'NONE',  ( 1.224646799147353700E-16, 0.000000000000000000, -1.000000000000000000 ) ) ;
#9814=ADVANCED_FACE ( 'NONE', ( #4478 ), #9259, .F. ) ;
#9818=DIRECTION ( 'NONE',  ( 0.000000000000000000, 1.000000000000000000, 0.000000000000000000 ) ) ;
#9821=ORIENTED_EDGE ( 'NONE', *, *, #3314, .F. ) ;
#9822=FACE_OUTER_BOUND ( 'NONE', #11038, .T. ) ;
#9836=TOROIDAL_SURFACE ( 'NONE', #10073, 0.5984251968503937480, 0.007874015748031495954 ) ;
#9837=VERTEX_POINT ( 'NONE', #3299 ) ;
#9839=AXIS2_PLACEMENT_3D ( 'NONE', #4807, #8270, #129 ) ;
#9847=AXIS2_PLACEMENT_3D ( 'NONE', #1703, #8910, #13917 ) ;
#9848=FACE_OUTER_BOUND ( 'NONE', #5490, .T. ) ;
#9849=DIRECTION ( 'NONE',  ( -1.224646799147353947E-16, 0.000000000000000000, -1.000000000000000000 ) ) ;
#9856=EDGE_LOOP ( 'NONE', ( #4752, #13104 ) ) ;
#9859=AXIS2_PLACEMENT_3D ( 'NONE', #12431, #6458, #10064 ) ;
#9872=DIRECTION ( 'NONE',  ( 0.000000000000000000, 1.000000000000000000, 0.000000000000000000 ) ) ;
#9873=DIRECTION ( 'NONE',  ( -0.000000000000000000, -0.000000000000000000, -1.000000000000000000 ) ) ;
#9874=CIRCLE ( 'NONE', #12374, 0.5905511811023621549 ) ;
#9875=AXIS2_PLACEMENT_3D ( 'NONE', #8567, #10926, #9768 ) ;
#9878=AXIS2_PLACEMENT_3D ( 'NONE', #7825, #11447, #2111 ) ;
#9883=ORIENTED_EDGE ( 'NONE', *, *, #5250, .T. ) ;
#9890=DIRECTION ( 'NONE',  ( 0.000000000000000000, 0.000000000000000000, -1.000000000000000000 ) ) ;
#9903=EDGE_LOOP ( 'NONE', ( #10802, #604, #10171, #4461 ) ) ;
#9905=VERTEX_POINT ( 'NONE', #11501 ) ;
#9910=DIRECTION ( 'NONE',  ( 0.000000000000000000, 0.000000000000000000, 1.000000000000000000 ) ) ;
#9914=CIRCLE ( 'NONE', #654, 0.6692913385826770867 ) ;
#9917=CARTESIAN_POINT ( 'NONE',  ( -0.06604848736013260724, 1.035433070866141891, -0.5868460571724354313 ) ) ;
#9921=DIRECTION ( 'NONE',  ( 0.000000000000000000, 0.000000000000000000, -1.000000000000000000 ) ) ;
#9922=ORIENTED_EDGE ( 'NONE', *, *, #7603, .T. ) ;
#9923=ADVANCED_FACE ( 'NONE', ( #6479 ), #698, .T. ) ;
#9930=AXIS2_PLACEMENT_3D ( 'NONE', #11858, #9346, #979 ) ;
#9935=EDGE_CURVE ( 'NONE', #5321, #14143, #14957, .T. ) ;
#9936=DIRECTION ( 'NONE',  ( -0.000000000000000000, -1.000000000000000000, -0.000000000000000000 ) ) ;
#9941=DIRECTION ( 'NONE',  ( 0.000000000000000000, 1.000000000000000000, 0.000000000000000000 ) ) ;
#9948=ORIENTED_EDGE ( 'NONE', *, *, #2251, .T. ) ;
#9952=DIRECTION ( 'NONE',  ( -0.000000000000000000, -1.000000000000000000, -0.000000000000000000 ) ) ;
#9962=AXIS2_PLACEMENT_3D ( 'NONE', #592, #10235, #12510 ) ;
#9963=DIRECTION ( 'NONE',  ( 0.000000000000000000, 0.000000000000000000, -1.000000000000000000 ) ) ;
#9974=DIRECTION ( 'NONE',  ( -0.8660254037844431485, 0.000000000000000000, -0.4999999999999918954 ) ) ;
#9975=DIRECTION ( 'NONE',  ( 0.000000000000000000, 0.000000000000000000, -1.000000000000000000 ) ) ;
#9976=LINE ( 'NONE', #8868, #14224 ) ;
#9979=AXIS2_PLACEMENT_3D ( 'NONE', #9493, #2340, #14332 ) ;
#10001=DIRECTION ( 'NONE',  ( 0.000000000000000000, 0.000000000000000000, -1.000000000000000000 ) ) ;
#10002=CARTESIAN_POINT ( 'NONE',  ( 0.4765556591343756976, 1.037732670558541903, 0.3487844890897296435 ) ) ;
#10004=CARTESIAN_POINT ( 'NONE',  ( 0.000000000000000000, 0.3622047244094487306, 0.000000000000000000 ) ) ;
#10008=CARTESIAN_POINT ( 'NONE',  ( 0.1181102362204724532, 2.637795275590551825, 0.03937007874015747977 ) ) ;
#10012=ORIENTED_EDGE ( 'NONE', *, *, #636, .T. ) ;
#10013=ORIENTED_EDGE ( 'NONE', *, *, #12581, .T. ) ;
#10014=EDGE_LOOP ( 'NONE', ( #6833, #4943 ) ) ;
#10020=CARTESIAN_POINT ( 'NONE',  ( 0.06278630405416070481, 1.038795175326500120, -0.5877245205702894548 ) ) ;
#10023=CYLINDRICAL_SURFACE ( 'NONE', #6168, 0.03937007874015751446 ) ;
#10024=CARTESIAN_POINT ( 'NONE',  ( -0.5450083523900178806, 1.338582677165354395, 0.2464697422870344434 ) ) ;
#10030=UNCERTAINTY_MEASURE_WITH_UNIT (LENGTH_MEASURE( 1.000000000000000082E-05 ), #12326, 'distance_accuracy_value', 'NONE');
#10044=ORIENTED_EDGE ( 'NONE', *, *, #4614, .F. ) ;
#10046=CARTESIAN_POINT ( 'NONE',  ( 0.000000000000000000, 1.653543307086614567, -0.5984251968503937480 ) ) ;
#10057=CARTESIAN_POINT ( 'NONE',  ( 0.000000000000000000, 1.377952755905512028, 0.7007874015748031260 ) ) ;
#10059=EDGE_CURVE ( 'NONE', #6809, #6855, #2194, .T. ) ;
#10062=ORIENTED_EDGE ( 'NONE', *, *, #10840, .T. ) ;
#10064=DIRECTION ( 'NONE',  ( 0.000000000000000000, 0.000000000000000000, 1.000000000000000000 ) ) ;
#10069=DIRECTION ( 'NONE',  ( 0.000000000000000000, -0.000000000000000000, -1.000000000000000000 ) ) ;
#10073=AXIS2_PLACEMENT_3D ( 'NONE', #8043, #2254, #15263 ) ;
#10079=ADVANCED_FACE ( 'NONE', ( #11660 ), #10637, .T. ) ;
#10086=AXIS2_PLACEMENT_3D ( 'NONE', #9662, #7222, #8311 ) ;
#10099=ORIENTED_EDGE ( 'NONE', *, *, #6234, .T. ) ;
#10103=AXIS2_PLACEMENT_3D ( 'NONE', #14750, #3927, #4069 ) ;
#10106=CARTESIAN_POINT ( 'NONE',  ( 0.000000000000000000, 0.5826771653543306728, -0.7086614173228346081 ) ) ;
#10114=AXIS2_PLACEMENT_3D ( 'NONE', #11940, #12015, #2285 ) ;
#10117=CYLINDRICAL_SURFACE ( 'NONE', #7669, 0.7086614173228346081 ) ;
#10120=CARTESIAN_POINT ( 'NONE',  ( -0.4859532342797812654, 1.338582677165354395, 0.3487562073009442543 ) ) ;
#10121=AXIS2_PLACEMENT_3D ( 'NONE', #545, #13854, #5296 ) ;
#10126=CARTESIAN_POINT ( 'NONE',  ( -0.05905511811023622659, 1.043307086614173151, -0.8267716535433072833 ) ) ;
#10128=AXIS2_PLACEMENT_3D ( 'NONE', #12794, #6915, #11710 ) ;
#10148=DIRECTION ( 'NONE',  ( 0.000000000000000000, 0.000000000000000000, -1.000000000000000000 ) ) ;
#10150=ORIENTED_EDGE ( 'NONE', *, *, #12210, .F. ) ;
#10158=CARTESIAN_POINT ( 'NONE',  ( -0.05905511811023622659, 1.190944881889763884, -0.8267716535433072833 ) ) ;
#10162=CARTESIAN_POINT ( 'NONE',  ( 0.000000000000000000, 1.338582677165354395, 0.000000000000000000 ) ) ;
#10171=ORIENTED_EDGE ( 'NONE', *, *, #378, .T. ) ;
#10172=CARTESIAN_POINT ( 'NONE',  ( 8.582170482213735190E-17, 1.645669291338583085, 0.7007874015748031260 ) ) ;
#10179=CIRCLE ( 'NONE', #680, 0.007874015748031516770 ) ;
#10194=CARTESIAN_POINT ( 'NONE',  ( 0.7114373258145217926, 1.190944881889763884, 0.3425575548946133142 ) ) ;
#10203=DIRECTION ( 'NONE',  ( 0.000000000000000000, -4.956352788505160310E-16, -1.000000000000000000 ) ) ;
#10213=EDGE_CURVE ( 'NONE', #9905, #851, #6061, .T. ) ;
#10217=CYLINDRICAL_SURFACE ( 'NONE', #6854, 0.007874015748031516770 ) ;
#10219=CARTESIAN_POINT ( 'NONE',  ( 0.000000000000000000, 1.614173228346457156, 0.6614173228346456046 ) ) ;
#10224=CARTESIAN_POINT ( 'NONE',  ( 0.4861941749621881415, 1.338582677165354395, 0.3488953144687809704 ) ) ;
#10228=CARTESIAN_POINT ( 'NONE',  ( 6.846450609406462919E-17, 0.5511811023622046335, -0.5590551181102362266 ) ) ;
#10235=DIRECTION ( 'NONE',  ( -0.5000000000000039968, 0.000000000000000000, -0.8660254037844362651 ) ) ;
#10239=DIRECTION ( 'NONE',  ( 0.000000000000000000, 0.000000000000000000, -1.000000000000000000 ) ) ;
#10243=VERTEX_POINT ( 'NONE', #11985 ) ;
#10246=CARTESIAN_POINT ( 'NONE',  ( -0.1574803149606299191, 0.03937007874015749365, 0.000000000000000000 ) ) ;
#10264=CARTESIAN_POINT ( 'NONE',  ( -0.4857119623810620679, 1.043292445042268257, 0.3486169089052708614 ) ) ;
#10268=EDGE_LOOP ( 'NONE', ( #2663, #4027, #6141, #11322 ) ) ;
#10270=CARTESIAN_POINT ( 'NONE',  ( 0.000000000000000000, 2.433070866141732846, 0.000000000000000000 ) ) ;
#10275=ORIENTED_EDGE ( 'NONE', *, *, #5551, .F. ) ;
#10276=EDGE_CURVE ( 'NONE', #10892, #7046, #5684, .T. ) ;
#10283=CARTESIAN_POINT ( 'NONE',  ( 0.000000000000000000, 0.000000000000000000, -0.1574803149606299191 ) ) ;
#10288=CARTESIAN_POINT ( 'NONE',  ( 0.000000000000000000, 0.04724409448818898960, 0.000000000000000000 ) ) ;
#10299=ADVANCED_FACE ( 'NONE', ( #12578 ), #9472, .F. ) ;
#10303=EDGE_CURVE ( 'NONE', #15395, #5700, #1841, .T. ) ;
#10308=ORIENTED_EDGE ( 'NONE', *, *, #10276, .T. ) ;
#10313=DIRECTION ( 'NONE',  ( 0.000000000000000000, 0.000000000000000000, 1.000000000000000000 ) ) ;
#10315=CARTESIAN_POINT ( 'NONE',  ( 6.750021727583836750E-17, 0.000000000000000000, 0.5511811023622046335 ) ) ;
#10318=FACE_OUTER_BOUND ( 'NONE', #6987, .T. ) ;
#10322=EDGE_LOOP ( 'NONE', ( #2980, #12547, #257, #8804 ) ) ;
#10325=AXIS2_PLACEMENT_3D ( 'NONE', #2179, #15330, #764 ) ;
#10327=DIRECTION ( 'NONE',  ( 0.000000000000000000, -0.000000000000000000, 1.000000000000000000 ) ) ;
#10328=VECTOR ( 'NONE', #5361, 39.37007874015748143 ) ;
#10332=DIRECTION ( 'NONE',  ( 0.000000000000000000, 0.000000000000000000, -1.000000000000000000 ) ) ;
#10335=DIRECTION ( 'NONE',  ( -0.000000000000000000, 1.000000000000000000, -0.000000000000000000 ) ) ;
#10340=ADVANCED_FACE ( 'NONE', ( #5443 ), #14972, .F. ) ;
#10342=ORIENTED_EDGE ( 'NONE', *, *, #11099, .F. ) ;
#10346=ORIENTED_EDGE ( 'NONE', *, *, #5551, .T. ) ;
#10347=EDGE_CURVE ( 'NONE', #15217, #14202, #11971, .T. ) ;
#10349=ORIENTED_EDGE ( 'NONE', *, *, #5832, .T. ) ;
#10354=AXIS2_PLACEMENT_3D ( 'NONE', #4154, #5009, #9808 ) ;
#10356=VECTOR ( 'NONE', #4627, 39.37007874015748143 ) ;
#10364=EDGE_CURVE ( 'NONE', #1922, #3058, #14780, .T. ) ;
#10368=CARTESIAN_POINT ( 'NONE',  ( 0.000000000000000000, 0.03937007874015749365, 0.000000000000000000 ) ) ;
#10370=AXIS2_PLACEMENT_3D ( 'NONE', #1863, #6299, #11187 ) ;
#10375=ORIENTED_EDGE ( 'NONE', *, *, #6616, .T. ) ;
#10377=VERTEX_POINT ( 'NONE', #11311 ) ;
#10387=CARTESIAN_POINT ( 'NONE',  ( 6.846450609406462919E-17, 1.417322834645669438, 0.5590551181102362266 ) ) ;
#10400=VERTEX_POINT ( 'NONE', #12810 ) ;
#10401=AXIS2_PLACEMENT_3D ( 'NONE', #1231, #13211, #13502 ) ;
#10402=ADVANCED_FACE ( 'NONE', ( #9288 ), #8108, .F. ) ;
#10408=DIRECTION ( 'NONE',  ( 0.8660254037844431485, -4.956352788505159323E-16, 0.4999999999999918954 ) ) ;
#10409=AXIS2_PLACEMENT_3D ( 'NONE', #12439, #6468, #7882 ) ;
#10412=ORIENTED_EDGE ( 'NONE', *, *, #780, .F. ) ;
#10415=DIRECTION ( 'NONE',  ( 0.000000000000000000, 0.000000000000000000, 1.000000000000000000 ) ) ;
#10416=TOROIDAL_SURFACE ( 'NONE', #7170, 0.7007874015748031260, 0.007874015748031495954 ) ;
#10417=ORIENTED_EDGE ( 'NONE', *, *, #3505, .F. ) ;
#10418=ORIENTED_EDGE ( 'NONE', *, *, #529, .T. ) ;
#10423=AXIS2_PLACEMENT_3D ( 'NONE', #12250, #13552, #9974 ) ;
#10432=AXIS2_PLACEMENT_3D ( 'NONE', #13419, #9818, #6197 ) ;
#10435=ORIENTED_EDGE ( 'NONE', *, *, #2774, .F. ) ;
#10436=CARTESIAN_POINT ( 'NONE',  ( 0.1181102362204724532, 2.637795275590551825, 0.03937007874015747977 ) ) ;
#10439=ORIENTED_EDGE ( 'NONE', *, *, #6170, .F. ) ;
#10442=CARTESIAN_POINT ( 'NONE',  ( 0.4854723491485768982, 1.043307086614173373, 0.3484785681409844904 ) ) ;
#10445=FACE_OUTER_BOUND ( 'NONE', #4460, .T. ) ;
#10446=CIRCLE ( 'NONE', #2694, 0.7007874015748031260 ) ;
#10455=ORIENTED_EDGE ( 'NONE', *, *, #7586, .F. ) ;
#10458=TOROIDAL_SURFACE ( 'NONE', #3214, 0.5984251968503937480, 0.007874015748031495954 ) ;
#10463=EDGE_CURVE ( 'NONE', #11432, #6409, #7947, .T. ) ;
#10469=ADVANCED_FACE ( 'NONE', ( #3326 ), #11556, .F. ) ;
#10473=DIRECTION ( 'NONE',  ( 0.000000000000000000, 0.000000000000000000, -1.000000000000000000 ) ) ;
#10476=AXIS2_PLACEMENT_3D ( 'NONE', #3687, #8464, #11685 ) ;
#10477=ORIENTED_EDGE ( 'NONE', *, *, #2906, .F. ) ;
#10483=CARTESIAN_POINT ( 'NONE',  ( 1.928577636452524610E-17, 0.03149606299212599769, 0.1574803149606299191 ) ) ;
#10493=ORIENTED_EDGE ( 'NONE', *, *, #11729, .F. ) ;
#10495=DIRECTION ( 'NONE',  ( -0.000000000000000000, -1.000000000000000000, -0.000000000000000000 ) ) ;
#10501=VERTEX_POINT ( 'NONE', #3257 ) ;
#10504=CARTESIAN_POINT ( 'NONE',  ( -0.5445274672588088505, 1.338626482899105241, 0.2461921031270815630 ) ) ;
#10508=ADVANCED_FACE ( 'NONE', ( #4430 ), #13953, .T. ) ;
#10511=ORIENTED_EDGE ( 'NONE', *, *, #13815, .F. ) ;
#10517=DIRECTION ( 'NONE',  ( 0.000000000000000000, 0.000000000000000000, -1.000000000000000000 ) ) ;
#10526=DIRECTION ( 'NONE',  ( 0.000000000000000000, 0.000000000000000000, -1.000000000000000000 ) ) ;
#10527=EDGE_CURVE ( 'NONE', #776, #13544, #458, .T. ) ;
#10532=EDGE_LOOP ( 'NONE', ( #3922, #3660 ) ) ;
#10549=EDGE_LOOP ( 'NONE', ( #2249, #14707, #761, #13631 ) ) ;
#10561=ADVANCED_FACE ( 'NONE', ( #11126 ), #326, .F. ) ;
#10564=EDGE_CURVE ( 'NONE', #6005, #2150, #8708, .T. ) ;
#10582=AXIS2_PLACEMENT_3D ( 'NONE', #14549, #8516, #13457 ) ;
#10585=EDGE_CURVE ( 'NONE', #5700, #9905, #3776, .T. ) ;
#10587=( BOUNDED_CURVE ( )  B_SPLINE_CURVE ( 3, ( #3312, #6753, #14283, #12874 ),
 .UNSPECIFIED., .F., .T. ) 
 B_SPLINE_CURVE_WITH_KNOTS ( ( 4, 4 ),
 ( 1.570796326794896558, 3.141592653589793116 ),
 .UNSPECIFIED. ) 
 CURVE ( )  GEOMETRIC_REPRESENTATION_ITEM ( )  RATIONAL_B_SPLINE_CURVE ( ( 1.000000000000000000, 0.8047378541243649375, 0.8047378541243649375, 1.000000000000000000 ) ) 
 REPRESENTATION_ITEM ( '' )  );
#10590=EDGE_CURVE ( 'NONE', #12965, #8519, #15220, .T. ) ;
#10600=AXIS2_PLACEMENT_3D ( 'NONE', #10270, #7831, #789 ) ;
#10609=CIRCLE ( 'NONE', #10103, 0.5511811023622046335 ) ;
#10610=ORIENTED_EDGE ( 'NONE', *, *, #3095, .F. ) ;
#10627=EDGE_LOOP ( 'NONE', ( #7055, #13955 ) ) ;
#10629=ORIENTED_EDGE ( 'NONE', *, *, #11002, .T. ) ;
#10632=VECTOR ( 'NONE', #4096, 39.37007874015748143 ) ;
#10637=CYLINDRICAL_SURFACE ( 'NONE', #1447, 0.7086614173228346081 ) ;
#10639=DIRECTION ( 'NONE',  ( -1.224646799147353947E-16, 0.000000000000000000, -1.000000000000000000 ) ) ;
#10640=ORIENTED_EDGE ( 'NONE', *, *, #8820, .F. ) ;
#10641=CARTESIAN_POINT ( 'NONE',  ( 0.000000000000000000, 0.000000000000000000, 0.000000000000000000 ) ) ;
#10647=ORIENTED_EDGE ( 'NONE', *, *, #8854, .F. ) ;
#10648=ORIENTED_EDGE ( 'NONE', *, *, #4848, .F. ) ;
#10650=ORIENTED_EDGE ( 'NONE', *, *, #1484, .T. ) ;
#10654=EDGE_CURVE ( 'NONE', #11417, #13359, #8978, .T. ) ;
#10658=LINE ( 'NONE', #4618, #2939 ) ;
#10662=EDGE_LOOP ( 'NONE', ( #6411, #3351 ) ) ;
#10676=EDGE_CURVE ( 'NONE', #2543, #13376, #7685, .T. ) ;
#10683=AXIS2_PLACEMENT_3D ( 'NONE', #7298, #201, #9752 ) ;
#10693=ORIENTED_EDGE ( 'NONE', *, *, #9517, .F. ) ;
#10695=ORIENTED_EDGE ( 'NONE', *, *, #2809, .F. ) ;
#10696=EDGE_LOOP ( 'NONE', ( #12750, #12505, #815, #2006 ) ) ;
#10700=CIRCLE ( 'NONE', #5680, 0.007874015748031449116 ) ;
#10707=ADVANCED_FACE ( 'NONE', ( #3223, #2031 ), #5401, .F. ) ;
#10714=CARTESIAN_POINT ( 'NONE',  ( -0.7455328141524870667, 1.338582677165354395, 0.3622425942647020669 ) ) ;
#10724=AXIS2_PLACEMENT_3D ( 'NONE', #769, #3206, #622 ) ;
#10728=ORIENTED_EDGE ( 'NONE', *, *, #1484, .F. ) ;
#10729=CARTESIAN_POINT ( 'NONE',  ( 0.000000000000000000, 0.007874015748031480341, 0.5826771653543306728 ) ) ;
#10732=DIRECTION ( 'NONE',  ( 0.000000000000000000, 0.000000000000000000, -1.000000000000000000 ) ) ;
#10734=DIRECTION ( 'NONE',  ( 0.000000000000000000, 0.000000000000000000, -1.000000000000000000 ) ) ;
#10738=CARTESIAN_POINT ( 'NONE',  ( -0.06012940348033157800, 1.340161119985692872, -0.5902917039295724200 ) ) ;
#10739=DIRECTION ( 'NONE',  ( 0.000000000000000000, 0.000000000000000000, -1.000000000000000000 ) ) ;
#10741=ORIENTED_EDGE ( 'NONE', *, *, #13739, .F. ) ;
#10751=CARTESIAN_POINT ( 'NONE',  ( 2.025006518275150778E-17, 0.007874015748031480341, -0.1653543307086614012 ) ) ;
#10761=EDGE_LOOP ( 'NONE', ( #4084, #4698 ) ) ;
#10763=ORIENTED_EDGE ( 'NONE', *, *, #3571, .F. ) ;
#10784=EDGE_CURVE ( 'NONE', #11091, #1695, #7867, .T. ) ;
#10786=FACE_OUTER_BOUND ( 'NONE', #473, .T. ) ;
#10789=FACE_OUTER_BOUND ( 'NONE', #1485, .T. ) ;
#10791=DIRECTION ( 'NONE',  ( -1.000000000000000000, 0.000000000000000000, 0.000000000000000000 ) ) ;
#10792=ORIENTED_EDGE ( 'NONE', *, *, #12282, .T. ) ;
#10793=VERTEX_POINT ( 'NONE', #13791 ) ;
#10797=ADVANCED_FACE ( 'NONE', ( #4469 ), #15118, .F. ) ;
#10799=CARTESIAN_POINT ( 'NONE',  ( 0.000000000000000000, 1.661417322834646049, 0.000000000000000000 ) ) ;
#10802=ORIENTED_EDGE ( 'NONE', *, *, #12484, .F. ) ;
#10803=CARTESIAN_POINT ( 'NONE',  ( 0.000000000000000000, 1.409448818897637956, -0.5590551181102362266 ) ) ;
#10805=ORIENTED_EDGE ( 'NONE', *, *, #14623, .F. ) ;
#10809=FACE_OUTER_BOUND ( 'NONE', #6058, .T. ) ;
#10818=TOROIDAL_SURFACE ( 'NONE', #9847, 0.5984251968503937480, 0.007874015748031495954 ) ;
#10819=DIRECTION ( 'NONE',  ( 2.664535259100375697E-15, 0.000000000000000000, -1.000000000000000000 ) ) ;
#10820=EDGE_CURVE ( 'NONE', #11532, #13926, #6198, .T. ) ;
#10823=VERTEX_POINT ( 'NONE', #6975 ) ;
#10824=ORIENTED_EDGE ( 'NONE', *, *, #1481, .T. ) ;
#10840=EDGE_CURVE ( 'NONE', #13129, #1428, #13472, .T. ) ;
#10844=AXIS2_PLACEMENT_3D ( 'NONE', #4428, #9215, #7720 ) ;
#10852=DIRECTION ( 'NONE',  ( 0.8660254037844362651, 0.000000000000000000, -0.5000000000000038858 ) ) ;
#10858=TOROIDAL_SURFACE ( 'NONE', #10121, 0.5826771653543306728, 0.007874015748031495954 ) ;
#10861=B_SPLINE_CURVE_WITH_KNOTS ( 'NONE', 3,
 ( #5834, #11750, #1013, #3441, #2253, #4690 ),
 .UNSPECIFIED., .F., .F.,
 ( 4, 2, 4 ),
 ( -2.828444569871933696E-06, 0.0001777364543001176602, 0.0003583013531701072511 ),
 .UNSPECIFIED. ) ;
#10865=EDGE_CURVE ( 'NONE', #6453, #562, #6457, .T. ) ;
#10867=CARTESIAN_POINT ( 'NONE',  ( 0.4859532342797860394, 1.043307086614173373, 0.3487562073009374264 ) ) ;
#10870=CIRCLE ( 'NONE', #9383, 0.007874015748031516770 ) ;
#10874=EDGE_CURVE ( 'NONE', #8556, #11565, #7185, .T. ) ;
#10880=CARTESIAN_POINT ( 'NONE',  ( -0.5445274672588088505, 1.043263280880422528, 0.2461921031270815630 ) ) ;
#10886=VERTEX_POINT ( 'NONE', #11765 ) ;
#10890=DIRECTION ( 'NONE',  ( 0.000000000000000000, 1.000000000000000000, 0.000000000000000000 ) ) ;
#10891=ORIENTED_EDGE ( 'NONE', *, *, #7160, .F. ) ;
#10892=VERTEX_POINT ( 'NONE', #11924 ) ;
#10902=CARTESIAN_POINT ( 'NONE',  ( -0.05905511811023622659, 1.043012312267831421, -0.5922897223582480608 ) ) ;
#10909=AXIS2_PLACEMENT_3D ( 'NONE', #2829, #7614, #12407 ) ;
#10914=ORIENTED_EDGE ( 'NONE', *, *, #8780, .F. ) ;
#10915=EDGE_LOOP ( 'NONE', ( #5166, #10439, #12445, #1424 ) ) ;
#10918=AXIS2_PLACEMENT_3D ( 'NONE', #5034, #5118, #1598 ) ;
#10926=DIRECTION ( 'NONE',  ( 0.000000000000000000, 1.000000000000000000, 0.000000000000000000 ) ) ;
#10929=CIRCLE ( 'NONE', #1434, 0.5984251968503937480 ) ;
#10931=EDGE_CURVE ( 'NONE', #677, #3049, #1725, .T. ) ;
#10933=AXIS2_PLACEMENT_3D ( 'NONE', #13226, #3, #8515 ) ;
#10935=ORIENTED_EDGE ( 'NONE', *, *, #5571, .F. ) ;
#10939=DIRECTION ( 'NONE',  ( -1.000000000000000000, 0.000000000000000000, 0.000000000000000000 ) ) ;
#10940=AXIS2_PLACEMENT_3D ( 'NONE', #4053, #13932, #477 ) ;
#10949=ADVANCED_FACE ( 'NONE', ( #9647 ), #14187, .F. ) ;
#10950=ORIENTED_EDGE ( 'NONE', *, *, #10958, .F. ) ;
#10956=CIRCLE ( 'NONE', #1222, 0.5984251968503937480 ) ;
#10958=EDGE_CURVE ( 'NONE', #10886, #15338, #5859, .T. ) ;
#10970=FACE_BOUND ( 'NONE', #9856, .T. ) ;
#10971=EDGE_LOOP ( 'NONE', ( #13017, #6792, #9127, #966 ) ) ;
#10973=EDGE_LOOP ( 'NONE', ( #1715, #4879, #3804, #13697, #1016, #2788, #13837, #827 ) ) ;
#10974=CARTESIAN_POINT ( 'NONE',  ( 0.000000000000000000, 1.377952755905512028, 0.000000000000000000 ) ) ;
#10975=EDGE_CURVE ( 'NONE', #9581, #2107, #6414, .T. ) ;
#10978=CARTESIAN_POINT ( 'NONE',  ( 0.06604848736013260724, 1.346456692913385877, -0.5868460571724354313 ) ) ;
#10980=CYLINDRICAL_SURFACE ( 'NONE', #695, 0.007874015748031516770 ) ;
#10981=DIRECTION ( 'NONE',  ( 0.000000000000000000, 0.000000000000000000, 1.000000000000000000 ) ) ;
#10989=FACE_OUTER_BOUND ( 'NONE', #14265, .T. ) ;
#10991=ORIENTED_EDGE ( 'NONE', *, *, #9517, .T. ) ;
#10994=CARTESIAN_POINT ( 'NONE',  ( 0.000000000000000000, 0.5826771653543306728, 0.000000000000000000 ) ) ;
#10995=CARTESIAN_POINT ( 'NONE',  ( 0.6864776960422569463, 1.043307086614173151, 0.4645290592786023298 ) ) ;
#10997=DIRECTION ( 'NONE',  ( 0.000000000000000000, 1.000000000000000000, 0.000000000000000000 ) ) ;
#11002=EDGE_CURVE ( 'NONE', #1695, #5321, #4465, .T. ) ;
#11004=CARTESIAN_POINT ( 'NONE',  ( -0.05905511811023622659, 1.190944881889763884, -0.8267716535433072833 ) ) ;
#11014=FACE_BOUND ( 'NONE', #8774, .T. ) ;
#11027=EDGE_CURVE ( 'NONE', #5052, #14569, #4433, .T. ) ;
#11038=EDGE_LOOP ( 'NONE', ( #14140, #13061, #10455, #10891 ) ) ;
#11045=ORIENTED_EDGE ( 'NONE', *, *, #2227, .T. ) ;
#11046=DIRECTION ( 'NONE',  ( -1.000000000000000000, 0.000000000000000000, 0.000000000000000000 ) ) ;
#11055=ORIENTED_EDGE ( 'NONE', *, *, #6917, .F. ) ;
#11056=EDGE_CURVE ( 'NONE', #6453, #2422, #12695, .T. ) ;
#11060=CARTESIAN_POINT ( 'NONE',  ( 0.000000000000000000, 0.5590551181102362266, 0.000000000000000000 ) ) ;
#11062=( LENGTH_UNIT ( ) NAMED_UNIT ( * ) SI_UNIT ( $, .METRE. ) );
#11063=CARTESIAN_POINT ( 'NONE',  ( 0.000000000000000000, 0.000000000000000000, 0.000000000000000000 ) ) ;
#11067=DIRECTION ( 'NONE',  ( 0.000000000000000000, 4.956352788505160310E-16, 1.000000000000000000 ) ) ;
#11070=AXIS2_PLACEMENT_3D ( 'NONE', #12686, #9157, #9477 ) ;
#11071=EDGE_LOOP ( 'NONE', ( #1179, #4832 ) ) ;
#11072=AXIS2_PLACEMENT_3D ( 'NONE', #375, #1250, #6003 ) ;
#11073=ADVANCED_FACE ( 'NONE', ( #7975 ), #7812, .F. ) ;
#11085=AXIS2_PLACEMENT_3D ( 'NONE', #135, #2625, #3799 ) ;
#11086=CARTESIAN_POINT ( 'NONE',  ( 0.000000000000000000, 0.3622047244094487306, 0.000000000000000000 ) ) ;
#11090=ORIENTED_EDGE ( 'NONE', *, *, #11607, .F. ) ;
#11091=VERTEX_POINT ( 'NONE', #5614 ) ;
#11092=VERTEX_POINT ( 'NONE', #13780 ) ;
#11098=VECTOR ( 'NONE', #9685, 39.37007874015748143 ) ;
#11099=EDGE_CURVE ( 'NONE', #8067, #2107, #15198, .T. ) ;
#11108=CIRCLE ( 'NONE', #7859, 0.007874015748031516770 ) ;
#11111=CARTESIAN_POINT ( 'NONE',  ( 6.750021727583836750E-17, 2.393700787401575436, 0.5511811023622046335 ) ) ;
#11113=ORIENTED_EDGE ( 'NONE', *, *, #11856, .F. ) ;
#11117=CARTESIAN_POINT ( 'NONE',  ( 0.000000000000000000, 1.622047244094488638, 0.5590551181102362266 ) ) ;
#11122=VECTOR ( 'NONE', #5976, 39.37007874015748143 ) ;
#11124=CYLINDRICAL_SURFACE ( 'NONE', #9878, 0.5905511811023621549 ) ;
#11126=FACE_OUTER_BOUND ( 'NONE', #3264, .T. ) ;
#11127=CIRCLE ( 'NONE', #15411, 0.007874015748031516770 ) ;
#11129=ORIENTED_EDGE ( 'NONE', *, *, #11461, .F. ) ;
#11139=ORIENTED_EDGE ( 'NONE', *, *, #2369, .T. ) ;
#11140=EDGE_CURVE ( 'NONE', #7200, #1180, #7900, .T. ) ;
#11143=FACE_BOUND ( 'NONE', #1444, .T. ) ;
#11161=CIRCLE ( 'NONE', #6396, 0.03937007874015751446 ) ;
#11165=FACE_OUTER_BOUND ( 'NONE', #13196, .T. ) ;
#11168=EDGE_CURVE ( 'NONE', #6389, #14049, #12603, .T. ) ;
#11175=EDGE_CURVE ( 'NONE', #4716, #10501, #8838, .T. ) ;
#11182=ORIENTED_EDGE ( 'NONE', *, *, #14203, .F. ) ;
#11187=DIRECTION ( 'NONE',  ( 1.000000000000000000, 0.000000000000000000, 0.000000000000000000 ) ) ;
#11188=AXIS2_PLACEMENT_3D ( 'NONE', #10641, #9627, #14548 ) ;
#11195=CARTESIAN_POINT ( 'NONE',  ( -0.4765664223158451174, 1.344138844425170731, 0.3487699017373184218 ) ) ;
#11200=AXIS2_PLACEMENT_3D ( 'NONE', #11589, #862, #14024 ) ;
#11203=ORIENTED_EDGE ( 'NONE', *, *, #8631, .T. ) ;
#11205=CIRCLE ( 'NONE', #7951, 0.007874015748031449116 ) ;
#11208=DIRECTION ( 'NONE',  ( -0.8660254037844363761, 0.000000000000000000, 0.5000000000000038858 ) ) ;
#11218=DIRECTION ( 'NONE',  ( 0.000000000000000000, 1.000000000000000000, 0.000000000000000000 ) ) ;
#11219=ADVANCED_FACE ( 'NONE', ( #9073 ), #571, .T. ) ;
#11220=DIRECTION ( 'NONE',  ( 0.000000000000000000, 1.000000000000000000, 0.000000000000000000 ) ) ;
#11222=AXIS2_PLACEMENT_3D ( 'NONE', #12002, #9412, #13074 ) ;
#11223=ORIENTED_EDGE ( 'NONE', *, *, #14866, .F. ) ;
#11224=EDGE_CURVE ( 'NONE', #4333, #7634, #4573, .T. ) ;
#11226=VERTEX_POINT ( 'NONE', #15334 ) ;
#11227=FACE_OUTER_BOUND ( 'NONE', #8051, .T. ) ;
#11231=DIRECTION ( 'NONE',  ( 0.000000000000000000, 0.000000000000000000, -1.000000000000000000 ) ) ;
#11235=CARTESIAN_POINT ( 'NONE',  ( 0.6864776960422567242, 1.338582677165354395, 0.4645290592786021633 ) ) ;
#11241=ADVANCED_FACE ( 'NONE', ( #15425 ), #8573, .F. ) ;
#11242=ORIENTED_EDGE ( 'NONE', *, *, #15218, .F. ) ;
#11250=DIRECTION ( 'NONE',  ( 0.000000000000000000, 0.000000000000000000, 1.000000000000000000 ) ) ;
#11256=ORIENTED_EDGE ( 'NONE', *, *, #9551, .T. ) ;
#11259=ORIENTED_EDGE ( 'NONE', *, *, #10347, .F. ) ;
#11262=ADVANCED_FACE ( 'NONE', ( #10786 ), #4760, .F. ) ;
#11283=VERTEX_POINT ( 'NONE', #3272 ) ;
#11284=DIRECTION ( 'NONE',  ( 0.000000000000000000, 1.000000000000000000, 0.000000000000000000 ) ) ;
#11285=PLANE ( 'NONE',  #3862 ) ;
#11290=EDGE_LOOP ( 'NONE', ( #1557, #4589, #1288, #8244 ) ) ;
#11292=DIRECTION ( 'NONE',  ( -0.000000000000000000, -1.000000000000000000, -0.000000000000000000 ) ) ;
#11299=EDGE_CURVE ( 'NONE', #2422, #14454, #13083, .T. ) ;
#11300=CARTESIAN_POINT ( 'NONE',  ( 0.000000000000000000, 1.346456692913385877, -0.5984251968503937480 ) ) ;
#11302=ORIENTED_EDGE ( 'NONE', *, *, #10590, .T. ) ;
#11306=ADVANCED_FACE ( 'NONE', ( #6871 ), #9836, .F. ) ;
#11311=CARTESIAN_POINT ( 'NONE',  ( 0.000000000000000000, 0.5984251968503937480, -0.5905511811023621549 ) ) ;
#11314=CARTESIAN_POINT ( 'NONE',  ( 0.000000000000000000, 0.3543307086614172485, -0.6614173228346456046 ) ) ;
#11322=ORIENTED_EDGE ( 'NONE', *, *, #1785, .T. ) ;
#11325=EDGE_CURVE ( 'NONE', #12382, #7799, #2562, .T. ) ;
#11342=ORIENTED_EDGE ( 'NONE', *, *, #4945, .F. ) ;
#11343=CARTESIAN_POINT ( 'NONE',  ( 0.05905511811023622659, 1.190944881889763884, -0.8267716535433072833 ) ) ;
#11353=ORIENTED_EDGE ( 'NONE', *, *, #12633, .T. ) ;
#11364=CARTESIAN_POINT ( 'NONE',  ( 0.000000000000000000, 1.035433070866142335, 0.000000000000000000 ) ) ;
#11365=AXIS2_PLACEMENT_3D ( 'NONE', #14659, #4938, #12156 ) ;
#11366=AXIS2_PLACEMENT_3D ( 'NONE', #2837, #1591, #7618 ) ;
#11371=EDGE_CURVE ( 'NONE', #115, #15219, #2721, .T. ) ;
#11374=CIRCLE ( 'NONE', #4619, 0.007874015748031482076 ) ;
#11376=AXIS2_PLACEMENT_3D ( 'NONE', #10246, #12682, #15029 ) ;
#11396=ORIENTED_EDGE ( 'NONE', *, *, #6917, .T. ) ;
#11397=CARTESIAN_POINT ( 'NONE',  ( 0.000000000000000000, 0.3622047244094487306, -0.6614173228346456046 ) ) ;
#11399=ORIENTED_EDGE ( 'NONE', *, *, #15011, .F. ) ;
#11401=AXIS2_PLACEMENT_3D ( 'NONE', #15022, #1709, #7962 ) ;
#11413=AXIS2_PLACEMENT_3D ( 'NONE', #13805, #3067, #7843 ) ;
#11414=ADVANCED_FACE ( 'NONE', ( #8582 ), #7318, .F. ) ;
#11417=VERTEX_POINT ( 'NONE', #4822 ) ;
#11418=AXIS2_PLACEMENT_3D ( 'NONE', #14447, #11046, #1213 ) ;
#11419=ORIENTED_EDGE ( 'NONE', *, *, #2369, .F. ) ;
#11423=FACE_BOUND ( 'NONE', #11071, .T. ) ;
#11426=CARTESIAN_POINT ( 'NONE',  ( 0.000000000000000000, 1.377952755905512028, 0.000000000000000000 ) ) ;
#11432=VERTEX_POINT ( 'NONE', #6288 ) ;
#11438=VERTEX_POINT ( 'NONE', #3743 ) ;
#11439=ORIENTED_EDGE ( 'NONE', *, *, #7165, .T. ) ;
#11445=DIRECTION ( 'NONE',  ( 0.000000000000000000, 1.000000000000000000, 0.000000000000000000 ) ) ;
#11447=DIRECTION ( 'NONE',  ( -0.000000000000000000, -1.000000000000000000, -0.000000000000000000 ) ) ;
#11448=DIRECTION ( 'NONE',  ( -0.000000000000000000, -1.000000000000000000, -0.000000000000000000 ) ) ;
#11454=CARTESIAN_POINT ( 'NONE',  ( -0.05905511811023625435, 2.637795275590551825, 0.03937007874015747977 ) ) ;
#11461=EDGE_CURVE ( 'NONE', #6519, #2195, #7326, .T. ) ;
#11468=CIRCLE ( 'NONE', #9721, 0.7007874015748031260 ) ;
#11470=DIRECTION ( 'NONE',  ( 0.000000000000000000, 0.000000000000000000, -1.000000000000000000 ) ) ;
#11471=CARTESIAN_POINT ( 'NONE',  ( -0.4815353412745563833, 0.000000000000000000, 0.3552976658085854056 ) ) ;
#11475=VERTEX_POINT ( 'NONE', #8674 ) ;
#11481=AXIS2_PLACEMENT_3D ( 'NONE', #12576, #4264, #5441 ) ;
#11484=EDGE_LOOP ( 'NONE', ( #3089, #2399 ) ) ;
#11498=CARTESIAN_POINT ( 'NONE',  ( -0.7455328141524873997, 1.190944881889763884, 0.3622425942647021779 ) ) ;
#11499=CARTESIAN_POINT ( 'NONE',  ( 3.379785373986856012E-18, 1.043307086614173596, 1.951319995474429431E-18 ) ) ;
#11501=CARTESIAN_POINT ( 'NONE',  ( 0.1181102362204724254, 2.448818897637795367, -0.03937007874015747977 ) ) ;
#11504=DIRECTION ( 'NONE',  ( 0.000000000000000000, 0.000000000000000000, 1.000000000000000000 ) ) ;
#11507=LINE ( 'NONE', #772, #3683 ) ;
#11510=DIRECTION ( 'NONE',  ( 1.000000000000000000, 0.000000000000000000, -1.224646799147353207E-16 ) ) ;
#11524=DIRECTION ( 'NONE',  ( 0.000000000000000000, 0.000000000000000000, 1.000000000000000000 ) ) ;
#11532=VERTEX_POINT ( 'NONE', #12435 ) ;
#11542=ADVANCED_FACE ( 'NONE', ( #2003 ), #10818, .F. ) ;
#11548=EDGE_CURVE ( 'NONE', #9404, #1672, #7327, .T. ) ;
#11554=B_SPLINE_CURVE_WITH_KNOTS ( 'NONE', 3,
 ( #9790, #8605, #6237, #12366 ),
 .UNSPECIFIED., .F., .F.,
 ( 4, 4 ),
 ( 0.000000000000000000, 2.119993237936687445E-05 ),
 .UNSPECIFIED. ) ;
#11556=CYLINDRICAL_SURFACE ( 'NONE', #1699, 0.03937007874015761161 ) ;
#11560=CARTESIAN_POINT ( 'NONE',  ( 7.328595018519593763E-17, 1.377952755905512028, -0.5984251968503937480 ) ) ;
#11565=VERTEX_POINT ( 'NONE', #11314 ) ;
#11576=CARTESIAN_POINT ( 'NONE',  ( 0.000000000000000000, 0.5590551181102362266, 0.000000000000000000 ) ) ;
#11577=FACE_OUTER_BOUND ( 'NONE', #10915, .T. ) ;
#11589=CARTESIAN_POINT ( 'NONE',  ( 0.000000000000000000, 1.417322834645669438, 0.000000000000000000 ) ) ;
#11590=DIRECTION ( 'NONE',  ( 0.000000000000000000, -0.000000000000000000, 1.000000000000000000 ) ) ;
#11592=ORIENTED_EDGE ( 'NONE', *, *, #5580, .F. ) ;
#11593=CARTESIAN_POINT ( 'NONE',  ( -0.05905511811023622659, 1.190944881889763884, -0.5946706712680680518 ) ) ;
#11594=DIRECTION ( 'NONE',  ( 0.000000000000000000, 0.000000000000000000, 1.000000000000000000 ) ) ;
#11606=ORIENTED_EDGE ( 'NONE', *, *, #13252, .F. ) ;
#11607=EDGE_CURVE ( 'NONE', #12818, #6858, #13687, .T. ) ;
#11608=DIRECTION ( 'NONE',  ( 0.000000000000000000, 1.000000000000000000, 0.000000000000000000 ) ) ;
#11610=AXIS2_PLACEMENT_3D ( 'NONE', #9005, #7809, #2700 ) ;
#11611=AXIS2_PLACEMENT_3D ( 'NONE', #5027, #1590, #8648 ) ;
#11624=DIRECTION ( 'NONE',  ( 0.000000000000000000, 1.000000000000000000, 0.000000000000000000 ) ) ;
#11625=ORIENTED_EDGE ( 'NONE', *, *, #12766, .T. ) ;
#11641=AXIS2_PLACEMENT_3D ( 'NONE', #7687, #14673, #1737 ) ;
#11643=DIRECTION ( 'NONE',  ( -8.673617379884029309E-17, -1.000000000000000000, 0.000000000000000000 ) ) ;
#11650=ORIENTED_EDGE ( 'NONE', *, *, #6147, .T. ) ;
#11651=CIRCLE ( 'NONE', #12160, 0.5826771653543306728 ) ;
#11655=EDGE_LOOP ( 'NONE', ( #13297, #8755, #11946, #2277 ) ) ;
#11660=FACE_OUTER_BOUND ( 'NONE', #10322, .T. ) ;
#11662=EDGE_CURVE ( 'NONE', #1599, #10400, #9094, .T. ) ;
#11664=AXIS2_PLACEMENT_3D ( 'NONE', #8514, #6155, #5045 ) ;
#11676=EDGE_LOOP ( 'NONE', ( #12091, #14282 ) ) ;
#11679=DIRECTION ( 'NONE',  ( 0.000000000000000000, 0.000000000000000000, 1.000000000000000000 ) ) ;
#11685=DIRECTION ( 'NONE',  ( 0.000000000000000000, 0.000000000000000000, 1.000000000000000000 ) ) ;
#11686=CARTESIAN_POINT ( 'NONE',  ( -0.05905511811023622659, 1.338582677165354395, -0.8267716535433070613 ) ) ;
#11689=CARTESIAN_POINT ( 'NONE',  ( -0.06604848736013260724, 1.346456692913385877, -0.5868460571724354313 ) ) ;
#11691=DIRECTION ( 'NONE',  ( -0.000000000000000000, -1.000000000000000000, -0.000000000000000000 ) ) ;
#11695=AXIS2_PLACEMENT_3D ( 'NONE', #12297, #14804, #1647 ) ;
#11696=ORIENTED_EDGE ( 'NONE', *, *, #7023, .T. ) ;
#11703=EDGE_CURVE ( 'NONE', #4548, #715, #12096, .T. ) ;
#11705=CYLINDRICAL_SURFACE ( 'NONE', #4611, 0.5905511811023621549 ) ;
#11708=AXIS2_PLACEMENT_3D ( 'NONE', #3247, #2057, #7373 ) ;
#11710=DIRECTION ( 'NONE',  ( 0.000000000000000000, 0.000000000000000000, -1.000000000000000000 ) ) ;
#11711=EDGE_LOOP ( 'NONE', ( #204, #6280, #8014, #15327 ) ) ;
#11720=ORIENTED_EDGE ( 'NONE', *, *, #10820, .F. ) ;
#11729=EDGE_CURVE ( 'NONE', #14746, #9379, #8839, .T. ) ;
#11732=AXIS2_PLACEMENT_3D ( 'NONE', #12545, #864, #11590 ) ;
#11737=CARTESIAN_POINT ( 'NONE',  ( -0.05905511811023622659, 1.043307086614173373, -0.5511811023622047445 ) ) ;
#11750=CARTESIAN_POINT ( 'NONE',  ( -0.5405798186813893791, 1.344775570699144218, 0.2377539613194186996 ) ) ;
#11765=CARTESIAN_POINT ( 'NONE',  ( -0.4751993499419962519, 1.346456692913385877, 0.3506226965216301950 ) ) ;
#11766=B_SPLINE_CURVE_WITH_KNOTS ( 'NONE', 3,
 ( #1109, #1976, #14030, #9325 ),
 .UNSPECIFIED., .F., .F.,
 ( 4, 4 ),
 ( 0.0001112824830758690162, 0.0003582764151311783850 ),
 .UNSPECIFIED. ) ;
#11769=DIRECTION ( 'NONE',  ( 4.292327424963298981E-16, -1.000000000000000000, -2.478176394252600369E-16 ) ) ;
#11777=VERTEX_POINT ( 'NONE', #7954 ) ;
#11779=CARTESIAN_POINT ( 'NONE',  ( 0.000000000000000000, 1.417322834645669438, 0.000000000000000000 ) ) ;
#11790=ORIENTED_EDGE ( 'NONE', *, *, #1481, .F. ) ;
#11796=EDGE_CURVE ( 'NONE', #7594, #25, #343, .T. ) ;
#11798=CARTESIAN_POINT ( 'NONE',  ( 7.183951695785653893E-17, -1.707404996040164512E-17, -0.5826771653543306728 ) ) ;
#11810=ORIENTED_EDGE ( 'NONE', *, *, #13998, .F. ) ;
#11812=EDGE_CURVE ( 'NONE', #2760, #677, #9591, .T. ) ;
#11817=DIRECTION ( 'NONE',  ( 0.000000000000000000, 0.000000000000000000, 1.000000000000000000 ) ) ;
#11819=DIRECTION ( 'NONE',  ( 0.000000000000000000, 1.000000000000000000, 0.000000000000000000 ) ) ;
#11827=CARTESIAN_POINT ( 'NONE',  ( 0.000000000000000000, 0.3464566929133857109, 0.000000000000000000 ) ) ;
#11834=CARTESIAN_POINT ( 'NONE',  ( 0.5424653753748086560, 1.043012296488531332, 0.2450015538227508782 ) ) ;
#11835=DIRECTION ( 'NONE',  ( 0.8660254037844362651, 0.000000000000000000, -0.5000000000000038858 ) ) ;
#11839=AXIS2_PLACEMENT_3D ( 'NONE', #13142, #2410, #1171 ) ;
#11841=VECTOR ( 'NONE', #3898, 39.37007874015748143 ) ;
#11854=VECTOR ( 'NONE', #595, 39.37007874015748143 ) ;
#11856=EDGE_CURVE ( 'NONE', #14202, #15217, #13340, .T. ) ;
#11857=VERTEX_POINT ( 'NONE', #11798 ) ;
#11858=CARTESIAN_POINT ( 'NONE',  ( 0.1259842519685039353, 2.448818897637795367, 0.03937007874015747977 ) ) ;
#11862=DIRECTION ( 'NONE',  ( -1.000000000000000000, 0.000000000000000000, 0.000000000000000000 ) ) ;
#11865=ORIENTED_EDGE ( 'NONE', *, *, #13815, .T. ) ;
#11870=ORIENTED_EDGE ( 'NONE', *, *, #1188, .F. ) ;
#11878=LINE ( 'NONE', #6045, #1113 ) ;
#11884=AXIS2_PLACEMENT_3D ( 'NONE', #721, #6888, #4230 ) ;
#11887=CIRCLE ( 'NONE', #5105, 0.007874015748031449116 ) ;
#11888=EDGE_LOOP ( 'NONE', ( #1561, #938, #6960, #9883 ) ) ;
#11892=ORIENTED_EDGE ( 'NONE', *, *, #8854, .T. ) ;
#11897=AXIS2_PLACEMENT_3D ( 'NONE', #3527, #8297, #9174 ) ;
#11902=CARTESIAN_POINT ( 'NONE',  ( 0.000000000000000000, 0.3070866141732283561, 0.000000000000000000 ) ) ;
#11912=EDGE_CURVE ( 'NONE', #9358, #6772, #103, .T. ) ;
#11914=AXIS2_PLACEMENT_3D ( 'NONE', #12367, #4217, #8835 ) ;
#11917=CIRCLE ( 'NONE', #12659, 0.1181102362204724532 ) ;
#11921=ADVANCED_FACE ( 'NONE', ( #1452 ), #12835, .T. ) ;
#11922=CARTESIAN_POINT ( 'NONE',  ( -0.1181102362204723977, 2.444206406002937815, -0.03937007874015747977 ) ) ;
#11924=CARTESIAN_POINT ( 'NONE',  ( 7.328595018519593763E-17, 0.5905511811023621549, 0.5984251968503937480 ) ) ;
#11927=EDGE_CURVE ( 'NONE', #6772, #9358, #1588, .T. ) ;
#11931=FACE_OUTER_BOUND ( 'NONE', #6294, .T. ) ;
#11932=ORIENTED_EDGE ( 'NONE', *, *, #12859, .F. ) ;
#11938=DIRECTION ( 'NONE',  ( 0.000000000000000000, 0.000000000000000000, -1.000000000000000000 ) ) ;
#11939=DIRECTION ( 'NONE',  ( -0.000000000000000000, -1.000000000000000000, -0.000000000000000000 ) ) ;
#11940=CARTESIAN_POINT ( 'NONE',  ( 0.000000000000000000, 1.370078740157480546, 0.000000000000000000 ) ) ;
#11944=CIRCLE ( 'NONE', #10432, 0.7086614173228346081 ) ;
#11946=ORIENTED_EDGE ( 'NONE', *, *, #9033, .F. ) ;
#11953=EDGE_CURVE ( 'NONE', #731, #12158, #8083, .T. ) ;
#11954=CIRCLE ( 'NONE', #440, 0.7007874015748031260 ) ;
#11961=ORIENTED_EDGE ( 'NONE', *, *, #9065, .F. ) ;
#11963=LINE ( 'NONE', #1225, #5830 ) ;
#11967=DIRECTION ( 'NONE',  ( -0.000000000000000000, -1.000000000000000000, -0.000000000000000000 ) ) ;
#11969=DIRECTION ( 'NONE',  ( -0.000000000000000000, -1.000000000000000000, -0.000000000000000000 ) ) ;
#11971=CIRCLE ( 'NONE', #9962, 0.03937007874015761855 ) ;
#11974=DIRECTION ( 'NONE',  ( 0.000000000000000000, -1.000000000000000000, 0.000000000000000000 ) ) ;
#11980=EDGE_CURVE ( 'NONE', #5700, #9010, #7469, .T. ) ;
#11985=CARTESIAN_POINT ( 'NONE',  ( -0.5452492930724200937, 1.338582677165354395, 0.2466088494548780152 ) ) ;
#11987=CARTESIAN_POINT ( 'NONE',  ( 7.328595018519593763E-17, 1.661417322834646049, 0.5984251968503937480 ) ) ;
#11992=CARTESIAN_POINT ( 'NONE',  ( 0.000000000000000000, 0.000000000000000000, -0.5905511811023621549 ) ) ;
#11998=FACE_BOUND ( 'NONE', #14507, .T. ) ;
#12002=CARTESIAN_POINT ( 'NONE',  ( 0.000000000000000000, 0.3543307086614172485, 0.000000000000000000 ) ) ;
#12008=ORIENTED_EDGE ( 'NONE', *, *, #4046, .F. ) ;
#12014=ADVANCED_FACE ( 'NONE', ( #12325 ), #13564, .F. ) ;
#12015=DIRECTION ( 'NONE',  ( -0.000000000000000000, -1.000000000000000000, -0.000000000000000000 ) ) ;
#12017=DIRECTION ( 'NONE',  ( -1.000000000000000000, -0.000000000000000000, -0.000000000000000000 ) ) ;
#12026=EDGE_CURVE ( 'NONE', #11417, #9358, #124, .T. ) ;
#12029=ORIENTED_EDGE ( 'NONE', *, *, #12633, .F. ) ;
#12038=CARTESIAN_POINT ( 'NONE',  ( 0.000000000000000000, 0.03937007874015749365, 0.000000000000000000 ) ) ;
#12040=CARTESIAN_POINT ( 'NONE',  ( -0.5450083523900178806, 1.043307086614173373, 0.2464697422870344157 ) ) ;
#12045=CARTESIAN_POINT ( 'NONE',  ( 0.05905511811023622659, 1.190944881889763884, -0.8661417322834648047 ) ) ;
#12049=CARTESIAN_POINT ( 'NONE',  ( 0.05905511811023622659, 1.190944881889763884, -0.8267716535433072833 ) ) ;
#12056=LINE ( 'NONE', #157, #13162 ) ;
#12064=CARTESIAN_POINT ( 'NONE',  ( 0.06440205152079661599, 1.037100910086407257, -0.5870313606185345590 ) ) ;
#12066=ORIENTED_EDGE ( 'NONE', *, *, #14856, .T. ) ;
#12075=CYLINDRICAL_SURFACE ( 'NONE', #2357, 0.5511811023622046335 ) ;
#12077=DIRECTION ( 'NONE',  ( 0.000000000000000000, 0.000000000000000000, 1.000000000000000000 ) ) ;
#12091=ORIENTED_EDGE ( 'NONE', *, *, #6721, .T. ) ;
#12095=TOROIDAL_SURFACE ( 'NONE', #3086, 0.6614173228346456046, 0.007874015748031495954 ) ;
#12096=CIRCLE ( 'NONE', #8850, 0.03937007874015751446 ) ;
#12097=TOROIDAL_SURFACE ( 'NONE', #8588, 0.5984251968503937480, 0.007874015748031495954 ) ;
#12099=DIRECTION ( 'NONE',  ( 0.000000000000000000, 1.000000000000000000, 0.000000000000000000 ) ) ;
#12106=CARTESIAN_POINT ( 'NONE',  ( 0.000000000000000000, 1.035433070866141891, -0.5905511811023621549 ) ) ;
#12107=ADVANCED_FACE ( 'NONE', ( #8971 ), #10217, .F. ) ;
#12110=CARTESIAN_POINT ( 'NONE',  ( 0.1213717603336464113, 2.440944881889763884, 0.04263160285333146560 ) ) ;
#12113=ORIENTED_EDGE ( 'NONE', *, *, #3396, .T. ) ;
#12114=AXIS2_PLACEMENT_3D ( 'NONE', #6415, #7449, #11208 ) ;
#12117=ORIENTED_EDGE ( 'NONE', *, *, #9273, .T. ) ;
#12119=CARTESIAN_POINT ( 'NONE',  ( 0.000000000000000000, 0.5984251968503937480, -0.5984251968503937480 ) ) ;
#12133=CARTESIAN_POINT ( 'NONE',  ( 0.4815353412745266848, 1.340095897400991554, 0.3474236500605469291 ) ) ;
#12135=ORIENTED_EDGE ( 'NONE', *, *, #13737, .T. ) ;
#12137=AXIS2_PLACEMENT_3D ( 'NONE', #1278, #7368, #1211 ) ;
#12138=CIRCLE ( 'NONE', #4905, 0.007874015748031449116 ) ;
#12139=ORIENTED_EDGE ( 'NONE', *, *, #12484, .T. ) ;
#12145=ADVANCED_FACE ( 'NONE', ( #13808 ), #13610, .F. ) ;
#12149=CIRCLE ( 'NONE', #11641, 0.5905511811023621549 ) ;
#12156=DIRECTION ( 'NONE',  ( 1.243449787580175325E-14, 4.625929269271485914E-16, 1.000000000000000000 ) ) ;
#12158=VERTEX_POINT ( 'NONE', #7936 ) ;
#12160=AXIS2_PLACEMENT_3D ( 'NONE', #2864, #13454, #11250 ) ;
#12162=ORIENTED_EDGE ( 'NONE', *, *, #4067, .F. ) ;
#12163=DIRECTION ( 'NONE',  ( 0.000000000000000000, 0.000000000000000000, -1.000000000000000000 ) ) ;
#12165=CARTESIAN_POINT ( 'NONE',  ( 0.4815353412745266848, 1.340095897400991554, 0.3474236500605469291 ) ) ;
#12174=AXIS2_PLACEMENT_3D ( 'NONE', #14550, #8753, #1399 ) ;
#12191=CYLINDRICAL_SURFACE ( 'NONE', #5350, 0.007874015748031482076 ) ;
#12192=CARTESIAN_POINT ( 'NONE',  ( 8.100026073100603114E-17, 0.5433070866141731514, -0.6614173228346456046 ) ) ;
#12193=EDGE_CURVE ( 'NONE', #15270, #381, #13092, .T. ) ;
#12194=DIRECTION ( 'NONE',  ( -0.000000000000000000, -1.000000000000000000, -0.000000000000000000 ) ) ;
#12196=FACE_BOUND ( 'NONE', #10627, .T. ) ;
#12199=ORIENTED_EDGE ( 'NONE', *, *, #3802, .F. ) ;
#12202=ADVANCED_FACE ( 'NONE', ( #7060 ), #11705, .T. ) ;
#12208=AXIS2_PLACEMENT_3D ( 'NONE', #2125, #6807, #8068 ) ;
#12210=EDGE_CURVE ( 'NONE', #9354, #15234, #9044, .T. ) ;
#12212=CARTESIAN_POINT ( 'NONE',  ( 0.000000000000000000, 0.000000000000000000, -0.5511811023622046335 ) ) ;
#12213=VECTOR ( 'NONE', #267, 39.37007874015748143 ) ;
#12216=CARTESIAN_POINT ( 'NONE',  ( 0.06604848736013260724, 1.346456692913385877, -0.5868460571724354313 ) ) ;
#12218=ORIENTED_EDGE ( 'NONE', *, *, #9029, .T. ) ;
#12231=FACE_OUTER_BOUND ( 'NONE', #6144, .T. ) ;
#12239=LINE ( 'NONE', #9798, #15224 ) ;
#12248=CARTESIAN_POINT ( 'NONE',  ( 0.1181102362204724254, 2.448818897637795367, 0.03937007874015747977 ) ) ;
#12250=CARTESIAN_POINT ( 'NONE',  ( 0.6864776960422569463, 1.190944881889763884, 0.4645290592786023298 ) ) ;
#12261=DIRECTION ( 'NONE',  ( 0.000000000000000000, 0.000000000000000000, 1.000000000000000000 ) ) ;
#12265=CARTESIAN_POINT ( 'NONE',  ( 0.000000000000000000, -1.707404996040164512E-17, 0.000000000000000000 ) ) ;
#12271=EDGE_CURVE ( 'NONE', #2247, #8826, #4108, .T. ) ;
#12274=CYLINDRICAL_SURFACE ( 'NONE', #3719, 0.7086614173228346081 ) ;
#12278=DIRECTION ( 'NONE',  ( -1.000000000000000000, 0.000000000000000000, 0.000000000000000000 ) ) ;
#12282=EDGE_CURVE ( 'NONE', #9905, #697, #8998, .T. ) ;
#12285=ORIENTED_EDGE ( 'NONE', *, *, #2904, .T. ) ;
#12286=ORIENTED_EDGE ( 'NONE', *, *, #116, .F. ) ;
#12288=ORIENTED_EDGE ( 'NONE', *, *, #5019, .F. ) ;
#12289=DIRECTION ( 'NONE',  ( -1.224646799147353947E-16, 0.000000000000000000, -1.000000000000000000 ) ) ;
#12290=CARTESIAN_POINT ( 'NONE',  ( 0.05905511811023622659, 1.190944881889763884, -0.8661417322834648047 ) ) ;
#12291=FACE_OUTER_BOUND ( 'NONE', #4375, .T. ) ;
#12292=CYLINDRICAL_SURFACE ( 'NONE', #4131, 0.1574803149606299191 ) ;
#12297=CARTESIAN_POINT ( 'NONE',  ( 0.000000000000000000, 0.000000000000000000, 0.000000000000000000 ) ) ;
#12298=ADVANCED_FACE ( 'NONE', ( #8313 ), #5883, .F. ) ;
#12303=EDGE_CURVE ( 'NONE', #5052, #10823, #6186, .T. ) ;
#12307=CARTESIAN_POINT ( 'NONE',  ( 8.678599364036360127E-17, 1.645669291338583085, 0.7086614173228346081 ) ) ;
#12314=CARTESIAN_POINT ( 'NONE',  ( 0.000000000000000000, 1.377952755905512028, 0.000000000000000000 ) ) ;
#12317=DIRECTION ( 'NONE',  ( 0.000000000000000000, 0.000000000000000000, -1.000000000000000000 ) ) ;
#12321=DIRECTION ( 'NONE',  ( -0.000000000000000000, -1.000000000000000000, -0.000000000000000000 ) ) ;
#12325=FACE_OUTER_BOUND ( 'NONE', #4150, .T. ) ;
#12326=( CONVERSION_BASED_UNIT ( 'INCH', #213 ) LENGTH_UNIT ( ) NAMED_UNIT ( #3471 ) );
#12327=DIRECTION ( 'NONE',  ( 0.000000000000000000, 1.000000000000000000, 0.000000000000000000 ) ) ;
#12328=CARTESIAN_POINT ( 'NONE',  ( -0.7455328141524873997, 1.190944881889763884, 0.3622425942647021779 ) ) ;
#12330=FACE_OUTER_BOUND ( 'NONE', #4001, .T. ) ;
#12332=VERTEX_POINT ( 'NONE', #12165 ) ;
#12333=AXIS2_PLACEMENT_3D ( 'NONE', #2283, #7142, #1205 ) ;
#12334=ORIENTED_EDGE ( 'NONE', *, *, #2878, .F. ) ;
#12336=ORIENTED_EDGE ( 'NONE', *, *, #15218, .T. ) ;
#12338=AXIS2_PLACEMENT_3D ( 'NONE', #4581, #5380, #13536 ) ;
#12339=DIRECTION ( 'NONE',  ( -0.8660254037844362651, 0.000000000000000000, 0.5000000000000041078 ) ) ;
#12345=VECTOR ( 'NONE', #7011, 39.37007874015748143 ) ;
#12348=CARTESIAN_POINT ( 'NONE',  ( 0.4828087445803718181, 1.042547362667152422, 0.3474236500605413780 ) ) ;
#12354=ORIENTED_EDGE ( 'NONE', *, *, #5282, .F. ) ;
#12363=B_SPLINE_CURVE_WITH_KNOTS ( 'NONE', 3,
 ( #6728, #4295, #5400, #14980 ),
 .UNSPECIFIED., .F., .F.,
 ( 4, 4 ),
 ( 0.000000000000000000, 0.0001112824830758690162 ),
 .UNSPECIFIED. ) ;
#12366=CARTESIAN_POINT ( 'NONE',  ( 0.5452492930724234244, 1.338582677165354395, 0.2466088494548705212 ) ) ;
#12367=CARTESIAN_POINT ( 'NONE',  ( 0.000000000000000000, 0.3622047244094487306, 0.000000000000000000 ) ) ;
#12371=VERTEX_POINT ( 'NONE', #10978 ) ;
#12374=AXIS2_PLACEMENT_3D ( 'NONE', #9724, #1550, #7665 ) ;
#12379=ORIENTED_EDGE ( 'NONE', *, *, #14303, .F. ) ;
#12380=CIRCLE ( 'NONE', #12625, 0.1476377952755906220 ) ;
#12381=ORIENTED_EDGE ( 'NONE', *, *, #10527, .T. ) ;
#12382=VERTEX_POINT ( 'NONE', #3841 ) ;
#12387=FACE_OUTER_BOUND ( 'NONE', #889, .T. ) ;
#12398=LINE ( 'NONE', #1742, #12716 ) ;
#12402=AXIS2_PLACEMENT_3D ( 'NONE', #2417, #10791, #71 ) ;
#12407=DIRECTION ( 'NONE',  ( 0.000000000000000000, 0.000000000000000000, -1.000000000000000000 ) ) ;
#12408=FACE_BOUND ( 'NONE', #10532, .T. ) ;
#12414=CIRCLE ( 'NONE', #11401, 0.5511811023622046335 ) ;
#12423=EDGE_LOOP ( 'NONE', ( #12135, #4605, #10044, #6489 ) ) ;
#12424=ORIENTED_EDGE ( 'NONE', *, *, #7823, .T. ) ;
#12425=EDGE_CURVE ( 'NONE', #10501, #2195, #14141, .T. ) ;
#12431=CARTESIAN_POINT ( 'NONE',  ( 0.000000000000000000, 0.5433070866141731514, 0.000000000000000000 ) ) ;
#12435=CARTESIAN_POINT ( 'NONE',  ( -0.6864776960422505070, 1.043307086614173151, 0.4645290592786119332 ) ) ;
#12437=CARTESIAN_POINT ( 'NONE',  ( 0.05905511811023622659, 1.338626482899105241, -0.5946706712680680518 ) ) ;
#12439=CARTESIAN_POINT ( 'NONE',  ( -0.5905511811023621549, 0.3149606299212598381, 0.000000000000000000 ) ) ;
#12442=ADVANCED_FACE ( 'NONE', ( #9087 ), #14903, .T. ) ;
#12445=ORIENTED_EDGE ( 'NONE', *, *, #7132, .T. ) ;
#12450=DIRECTION ( 'NONE',  ( 1.000000000000000000, 0.000000000000000000, -1.224646799147353207E-16 ) ) ;
#12458=DIRECTION ( 'NONE',  ( 0.000000000000000000, 1.000000000000000000, 0.000000000000000000 ) ) ;
#12461=VERTEX_POINT ( 'NONE', #10194 ) ;
#12475=DIRECTION ( 'NONE',  ( -1.000000000000000000, 0.000000000000000000, 0.000000000000000000 ) ) ;
#12484=EDGE_CURVE ( 'NONE', #11857, #9358, #1880, .T. ) ;
#12485=VERTEX_POINT ( 'NONE', #1969 ) ;
#12489=CARTESIAN_POINT ( 'NONE',  ( 0.000000000000000000, 0.000000000000000000, 0.000000000000000000 ) ) ;
#12490=DIRECTION ( 'NONE',  ( 0.5000000000000041078, 0.000000000000000000, 0.8660254037844362651 ) ) ;
#12495=DIRECTION ( 'NONE',  ( 0.000000000000000000, 1.000000000000000000, 0.000000000000000000 ) ) ;
#12496=DIRECTION ( 'NONE',  ( -0.000000000000000000, -1.000000000000000000, -0.000000000000000000 ) ) ;
#12504=DIRECTION ( 'NONE',  ( -0.000000000000000000, -1.000000000000000000, -0.000000000000000000 ) ) ;
#12505=ORIENTED_EDGE ( 'NONE', *, *, #6763, .F. ) ;
#12507=EDGE_CURVE ( 'NONE', #5799, #5070, #3419, .T. ) ;
#12510=DIRECTION ( 'NONE',  ( -0.8660254037844363761, 0.000000000000000000, 0.5000000000000038858 ) ) ;
#12515=DIRECTION ( 'NONE',  ( 0.000000000000000000, 0.000000000000000000, -1.000000000000000000 ) ) ;
#12519=ORIENTED_EDGE ( 'NONE', *, *, #15172, .F. ) ;
#12520=ORIENTED_EDGE ( 'NONE', *, *, #4615, .T. ) ;
#12521=ORIENTED_EDGE ( 'NONE', *, *, #11056, .F. ) ;
#12522=EDGE_CURVE ( 'NONE', #5070, #8722, #12363, .T. ) ;
#12531=CYLINDRICAL_SURFACE ( 'NONE', #7383, 0.6692913385826770867 ) ;
#12534=ORIENTED_EDGE ( 'NONE', *, *, #7700, .T. ) ;
#12536=CARTESIAN_POINT ( 'NONE',  ( -0.1259842519685039353, 2.440944881889763884, -0.03937007874015747977 ) ) ;
#12545=CARTESIAN_POINT ( 'NONE',  ( -0.5905511811023622659, 1.377952755905512028, 0.000000000000000000 ) ) ;
#12547=ORIENTED_EDGE ( 'NONE', *, *, #5013, .T. ) ;
#12549=CARTESIAN_POINT ( 'NONE',  ( -0.4854723491485721798, 1.338626482899105241, 0.3484785681409913738 ) ) ;
#12550=DIRECTION ( 'NONE',  ( 0.8660254037844433705, 0.000000000000000000, 0.4999999999999918954 ) ) ;
#12553=ORIENTED_EDGE ( 'NONE', *, *, #693, .F. ) ;
#12563=ORIENTED_EDGE ( 'NONE', *, *, #4159, .T. ) ;
#12571=ORIENTED_EDGE ( 'NONE', *, *, #5306, .T. ) ;
#12574=CARTESIAN_POINT ( 'NONE',  ( 0.05905511811023622659, 1.338582677165354395, -0.8267716535433070613 ) ) ;
#12576=CARTESIAN_POINT ( 'NONE',  ( 0.000000000000000000, 0.000000000000000000, 0.000000000000000000 ) ) ;
#12578=FACE_OUTER_BOUND ( 'NONE', #4590, .T. ) ;
#12581=EDGE_CURVE ( 'NONE', #8791, #6293, #1100, .T. ) ;
#12582=DIRECTION ( 'NONE',  ( -0.000000000000000000, 0.000000000000000000, -1.000000000000000000 ) ) ;
#12587=CIRCLE ( 'NONE', #5811, 0.5984251968503937480 ) ;
#12596=AXIS2_PLACEMENT_3D ( 'NONE', #14530, #3791, #433 ) ;
#12598=CIRCLE ( 'NONE', #3102, 0.5984251968503937480 ) ;
#12601=CIRCLE ( 'NONE', #1098, 0.007874015748031449116 ) ;
#12603=LINE ( 'NONE', #7668, #482 ) ;
#12608=EDGE_CURVE ( 'NONE', #288, #11417, #5867, .T. ) ;
#12611=AXIS2_PLACEMENT_3D ( 'NONE', #4817, #3888, #9612 ) ;
#12613=CIRCLE ( 'NONE', #12114, 0.03937007874015761855 ) ;
#12614=EDGE_CURVE ( 'NONE', #10501, #13129, #1144, .T. ) ;
#12615=AXIS2_PLACEMENT_3D ( 'NONE', #15341, #3585, #1018 ) ;
#12617=CYLINDRICAL_SURFACE ( 'NONE', #11884, 0.6692913385826770867 ) ;
#12619=AXIS2_PLACEMENT_3D ( 'NONE', #13847, #9155, #10313 ) ;
#12625=AXIS2_PLACEMENT_3D ( 'NONE', #325, #5079, #13547 ) ;
#12633=EDGE_CURVE ( 'NONE', #11438, #731, #11887, .T. ) ;
#12635=ORIENTED_EDGE ( 'NONE', *, *, #13737, .F. ) ;
#12639=CARTESIAN_POINT ( 'NONE',  ( -0.5452492930724200937, 1.043307086614173373, 0.2466088494548779875 ) ) ;
#12642=CARTESIAN_POINT ( 'NONE',  ( 0.000000000000000000, 1.346456692913385877, 0.000000000000000000 ) ) ;
#12647=CYLINDRICAL_SURFACE ( 'NONE', #5644, 0.03937007874015761855 ) ;
#12651=CIRCLE ( 'NONE', #12402, 0.007874015748031449116 ) ;
#12655=DIRECTION ( 'NONE',  ( -0.8660254037844431485, 0.000000000000000000, -0.4999999999999918954 ) ) ;
#12657=EDGE_CURVE ( 'NONE', #12827, #1436, #3217, .T. ) ;
#12659=AXIS2_PLACEMENT_3D ( 'NONE', #7551, #5275, #12278 ) ;
#12681=CARTESIAN_POINT ( 'NONE',  ( 8.678599364036360127E-17, 0.3228346456692913757, 0.7086614173228346081 ) ) ;
#12682=DIRECTION ( 'NONE',  ( 0.000000000000000000, -1.000000000000000000, -0.000000000000000000 ) ) ;
#12685=DIRECTION ( 'NONE',  ( 1.000000000000000000, -0.000000000000000000, 1.224646799147353207E-16 ) ) ;
#12686=CARTESIAN_POINT ( 'NONE',  ( 0.000000000000000000, 0.3543307086614172485, 0.000000000000000000 ) ) ;
#12691=FACE_OUTER_BOUND ( 'NONE', #560, .T. ) ;
#12693=ORIENTED_EDGE ( 'NONE', *, *, #8039, .T. ) ;
#12695=CIRCLE ( 'NONE', #5201, 0.5984251968503937480 ) ;
#12696=VECTOR ( 'NONE', #5638, 39.37007874015748143 ) ;
#12699=ORIENTED_EDGE ( 'NONE', *, *, #447, .T. ) ;
#12703=CIRCLE ( 'NONE', #14463, 0.007874015748031516770 ) ;
#12706=CARTESIAN_POINT ( 'NONE',  ( -0.4861941749621833675, 1.043307086614173373, 0.3488953144687877983 ) ) ;
#12707=CARTESIAN_POINT ( 'NONE',  ( 0.000000000000000000, 0.3070866141732283561, 0.5984251968503937480 ) ) ;
#12714=ADVANCED_FACE ( 'NONE', ( #8526 ), #12292, .F. ) ;
#12715=CARTESIAN_POINT ( 'NONE',  ( 7.328595018519593763E-17, 1.370078740157480546, -0.5984251968503937480 ) ) ;
#12716=VECTOR ( 'NONE', #10203, 39.37007874015748143 ) ;
#12721=ORIENTED_EDGE ( 'NONE', *, *, #1388, .T. ) ;
#12722=ORIENTED_EDGE ( 'NONE', *, *, #4351, .F. ) ;
#12723=VECTOR ( 'NONE', #9890, 39.37007874015748143 ) ;
#12728=LINE ( 'NONE', #10283, #15376 ) ;
#12730=DIRECTION ( 'NONE',  ( 0.000000000000000000, 1.000000000000000000, 0.000000000000000000 ) ) ;
#12733=FACE_OUTER_BOUND ( 'NONE', #6789, .T. ) ;
#12736=VECTOR ( 'NONE', #15189, 39.37007874015748143 ) ;
#12740=DIRECTION ( 'NONE',  ( 0.8660254037844433705, 0.000000000000000000, 0.4999999999999918954 ) ) ;
#12750=ORIENTED_EDGE ( 'NONE', *, *, #8636, .F. ) ;
#12754=VERTEX_POINT ( 'NONE', #14422 ) ;
#12762=ORIENTED_EDGE ( 'NONE', *, *, #4321, .T. ) ;
#12763=CARTESIAN_POINT ( 'NONE',  ( 0.000000000000000000, 1.370078740157480546, -0.5905511811023621549 ) ) ;
#12766=EDGE_CURVE ( 'NONE', #9167, #1544, #6622, .T. ) ;
#12769=CARTESIAN_POINT ( 'NONE',  ( -0.4478092776764608374, 1.043307086614173373, 0.3267337836880595536 ) ) ;
#12775=ORIENTED_EDGE ( 'NONE', *, *, #7746, .T. ) ;
#12776=LINE ( 'NONE', #11593, #2175 ) ;
#12777=DIRECTION ( 'NONE',  ( -1.000000000000000000, 0.000000000000000000, 0.000000000000000000 ) ) ;
#12781=ADVANCED_FACE ( 'NONE', ( #14651 ), #13139, .F. ) ;
#12783=ADVANCED_FACE ( 'NONE', ( #3991 ), #12531, .F. ) ;
#12784=EDGE_LOOP ( 'NONE', ( #3716, #12139, #9062, #5632 ) ) ;
#12785=ORIENTED_EDGE ( 'NONE', *, *, #14962, .T. ) ;
#12794=CARTESIAN_POINT ( 'NONE',  ( 0.000000000000000000, 1.338582677165354395, 0.000000000000000000 ) ) ;
#12810=CARTESIAN_POINT ( 'NONE',  ( 0.000000000000000000, 2.401574803149606918, 0.5433070866141731514 ) ) ;
#12816=B_SPLINE_CURVE_WITH_KNOTS ( 'NONE', 3,
 ( #2514, #13091, #13022, #7288, #10902, #190 ),
 .UNSPECIFIED., .F., .F.,
 ( 4, 2, 4 ),
 ( -2.828444569877115420E-06, 0.0001777364543001118868, 0.0003583013531701008544 ),
 .UNSPECIFIED. ) ;
#12818=VERTEX_POINT ( 'NONE', #4055 ) ;
#12822=DIRECTION ( 'NONE',  ( 0.000000000000000000, 0.000000000000000000, -1.000000000000000000 ) ) ;
#12823=CARTESIAN_POINT ( 'NONE',  ( 0.05905511811023622659, 1.338597318737259734, -0.5949473527966270270 ) ) ;
#12827=VERTEX_POINT ( 'NONE', #8764 ) ;
#12829=FACE_OUTER_BOUND ( 'NONE', #3520, .T. ) ;
#12834=AXIS2_PLACEMENT_3D ( 'NONE', #96, #14204, #15373 ) ;
#12835=TOROIDAL_SURFACE ( 'NONE', #3834, 0.5590551181102362266, 0.007874015748031495954 ) ;
#12836=EDGE_CURVE ( 'NONE', #1428, #13129, #644, .T. ) ;
#12850=CARTESIAN_POINT ( 'NONE',  ( -0.05905511811023622659, 1.338597318737259734, -0.5949473527966270270 ) ) ;
#12857=VERTEX_POINT ( 'NONE', #14879 ) ;
#12859=EDGE_CURVE ( 'NONE', #8791, #1599, #11127, .T. ) ;
#12860=EDGE_LOOP ( 'NONE', ( #4260, #12945, #10375, #15393, #8475, #11720 ) ) ;
#12867=DIRECTION ( 'NONE',  ( -0.000000000000000000, -1.000000000000000000, -0.000000000000000000 ) ) ;
#12874=CARTESIAN_POINT ( 'NONE',  ( -0.1181102362204724254, 2.448818897637795367, 0.03937007874015747977 ) ) ;
#12879=AXIS2_PLACEMENT_3D ( 'NONE', #2767, #12495, #7536 ) ;
#12883=VERTEX_POINT ( 'NONE', #1790 ) ;
#12888=ORIENTED_EDGE ( 'NONE', *, *, #252, .F. ) ;
#12889=VERTEX_POINT ( 'NONE', #9006 ) ;
#12896=CIRCLE ( 'NONE', #4383, 0.007874015748031516770 ) ;
#12900=EDGE_CURVE ( 'NONE', #14427, #776, #3043, .T. ) ;
#12905=AXIS2_PLACEMENT_3D ( 'NONE', #7959, #13918, #9142 ) ;
#12916=CIRCLE ( 'NONE', #12174, 0.1653543307086614012 ) ;
#12932=DIRECTION ( 'NONE',  ( 0.8660254037844363761, 0.000000000000000000, -0.5000000000000039968 ) ) ;
#12934=EDGE_LOOP ( 'NONE', ( #14290, #10914, #4815, #1040 ) ) ;
#12941=LINE ( 'NONE', #10436, #12696 ) ;
#12945=ORIENTED_EDGE ( 'NONE', *, *, #12507, .T. ) ;
#12951=DIRECTION ( 'NONE',  ( -0.000000000000000000, -1.000000000000000000, -0.000000000000000000 ) ) ;
#12952=DIRECTION ( 'NONE',  ( 0.000000000000000000, 0.000000000000000000, -1.000000000000000000 ) ) ;
#12954=CARTESIAN_POINT ( 'NONE',  ( 0.000000000000000000, 0.000000000000000000, 0.000000000000000000 ) ) ;
#12955=AXIS2_PLACEMENT_3D ( 'NONE', #9443, #3485, #15387 ) ;
#12964=AXIS2_PLACEMENT_3D ( 'NONE', #3183, #15168, #8481 ) ;
#12965=VERTEX_POINT ( 'NONE', #7974 ) ;
#12968=ORIENTED_EDGE ( 'NONE', *, *, #15282, .T. ) ;
#12971=VERTEX_POINT ( 'NONE', #5613 ) ;
#12973=DIRECTION ( 'NONE',  ( 0.000000000000000000, 0.000000000000000000, -1.000000000000000000 ) ) ;
#12987=EDGE_LOOP ( 'NONE', ( #9948, #4751 ) ) ;
#12988=ORIENTED_EDGE ( 'NONE', *, *, #6646, .F. ) ;
#12995=DIRECTION ( 'NONE',  ( 0.000000000000000000, 0.000000000000000000, 1.000000000000000000 ) ) ;
#13005=EDGE_CURVE ( 'NONE', #7918, #2233, #15141, .T. ) ;
#13009=CARTESIAN_POINT ( 'NONE',  ( 0.000000000000000000, 0.5511811023622046335, 0.000000000000000000 ) ) ;
#13017=ORIENTED_EDGE ( 'NONE', *, *, #10654, .T. ) ;
#13022=CARTESIAN_POINT ( 'NONE',  ( -0.06278592661683282672, 1.038795580266492768, -0.5877247716201635663 ) ) ;
#13026=DIRECTION ( 'NONE',  ( -0.4999999999999919509, 0.000000000000000000, 0.8660254037844432595 ) ) ;
#13032=ORIENTED_EDGE ( 'NONE', *, *, #7746, .F. ) ;
#13035=ORIENTED_EDGE ( 'NONE', *, *, #9935, .T. ) ;
#13039=EDGE_CURVE ( 'NONE', #563, #2898, #10861, .T. ) ;
#13040=CARTESIAN_POINT ( 'NONE',  ( 0.000000000000000000, 0.5826771653543306728, 0.000000000000000000 ) ) ;
#13049=EDGE_LOOP ( 'NONE', ( #11302, #9922 ) ) ;
#13061=ORIENTED_EDGE ( 'NONE', *, *, #11325, .T. ) ;
#13064=DIRECTION ( 'NONE',  ( -0.000000000000000000, -1.000000000000000000, -0.000000000000000000 ) ) ;
#13073=EDGE_CURVE ( 'NONE', #6404, #7200, #13156, .T. ) ;
#13074=DIRECTION ( 'NONE',  ( 0.000000000000000000, 0.000000000000000000, -1.000000000000000000 ) ) ;
#13079=CARTESIAN_POINT ( 'NONE',  ( 0.000000000000000000, 1.653543307086614567, 0.000000000000000000 ) ) ;
#13080=DIRECTION ( 'NONE',  ( -0.8660254037844431485, 0.000000000000000000, -0.4999999999999918954 ) ) ;
#13081=ORIENTED_EDGE ( 'NONE', *, *, #5187, .T. ) ;
#13083=CIRCLE ( 'NONE', #14584, 0.007874015748031516770 ) ;
#13089=CARTESIAN_POINT ( 'NONE',  ( 0.06692913385826772255, 0.000000000000000000, -0.5946706712680680518 ) ) ;
#13091=CARTESIAN_POINT ( 'NONE',  ( -0.06438893898759022461, 1.037114193080275637, -0.5870328364109900221 ) ) ;
#13092=LINE ( 'NONE', #3624, #1115 ) ;
#13096=VERTEX_POINT ( 'NONE', #2548 ) ;
#13099=TOROIDAL_SURFACE ( 'NONE', #6319, 0.7007874015748031260, 0.007874015748031495954 ) ;
#13104=ORIENTED_EDGE ( 'NONE', *, *, #693, .T. ) ;
#13105=EDGE_LOOP ( 'NONE', ( #2912, #15123, #8285, #2646 ) ) ;
#13111=ORIENTED_EDGE ( 'NONE', *, *, #2440, .F. ) ;
#13112=TOROIDAL_SURFACE ( 'NONE', #6595, 0.7007874015748031260, 0.007874015748031495954 ) ;
#13115=DIRECTION ( 'NONE',  ( 0.000000000000000000, 1.000000000000000000, 0.000000000000000000 ) ) ;
#13121=AXIS2_PLACEMENT_3D ( 'NONE', #13468, #7505, #2795 ) ;
#13127=AXIS2_PLACEMENT_3D ( 'NONE', #3054, #11448, #14811 ) ;
#13129=VERTEX_POINT ( 'NONE', #65 ) ;
#13130=EDGE_LOOP ( 'NONE', ( #10418, #11203 ) ) ;
#13133=EDGE_LOOP ( 'NONE', ( #5261, #5916, #14040, #13878 ) ) ;
#13139=TOROIDAL_SURFACE ( 'NONE', #11914, 0.6614173228346456046, 0.007874015748031495954 ) ;
#13142=CARTESIAN_POINT ( 'NONE',  ( 0.6864776960422567242, 1.338582677165354395, 0.4645290592786021633 ) ) ;
#13143=CARTESIAN_POINT ( 'NONE',  ( 0.05905511811023622659, 1.043307086614173373, -0.5955041639236610118 ) ) ;
#13145=CARTESIAN_POINT ( 'NONE',  ( 0.000000000000000000, 0.03149606299212599769, -0.1574803149606299191 ) ) ;
#13156=CIRCLE ( 'NONE', #15421, 0.1476377952755906775 ) ;
#13159=FACE_OUTER_BOUND ( 'NONE', #12987, .T. ) ;
#13162=VECTOR ( 'NONE', #4918, 39.37007874015748143 ) ;
#13163=DIRECTION ( 'NONE',  ( -0.5000000000000039968, 0.000000000000000000, -0.8660254037844362651 ) ) ;
#13167=AXIS2_PLACEMENT_3D ( 'NONE', #12192, #13434, #2701 ) ;
#13169=ORIENTED_EDGE ( 'NONE', *, *, #9226, .F. ) ;
#13172=CARTESIAN_POINT ( 'NONE',  ( -0.7455328141524870667, 1.338582677165354395, 0.3622425942647020669 ) ) ;
#13175=ORIENTED_EDGE ( 'NONE', *, *, #7165, .F. ) ;
#13177=EDGE_CURVE ( 'NONE', #381, #6293, #1649, .T. ) ;
#13182=DIRECTION ( 'NONE',  ( 0.000000000000000000, 0.000000000000000000, -1.000000000000000000 ) ) ;
#13187=TOROIDAL_SURFACE ( 'NONE', #10683, 0.5984251968503937480, 0.007874015748031495954 ) ;
#13188=DIRECTION ( 'NONE',  ( 0.000000000000000000, 0.000000000000000000, 1.000000000000000000 ) ) ;
#13196=EDGE_LOOP ( 'NONE', ( #7162, #13459, #10346, #15181 ) ) ;
#13198=AXIS2_PLACEMENT_3D ( 'NONE', #4934, #2500, #1326 ) ;
#13204=AXIS2_PLACEMENT_3D ( 'NONE', #14251, #11819, #232 ) ;
#13211=DIRECTION ( 'NONE',  ( -0.000000000000000000, -0.000000000000000000, -1.000000000000000000 ) ) ;
#13214=CARTESIAN_POINT ( 'NONE',  ( 0.1259842519685039353, 2.440944881889763884, 0.04724409448818898266 ) ) ;
#13226=CARTESIAN_POINT ( 'NONE',  ( 0.000000000000000000, 1.606299212598425674, 0.000000000000000000 ) ) ;
#13233=DIRECTION ( 'NONE',  ( -0.000000000000000000, -1.000000000000000000, -0.000000000000000000 ) ) ;
#13245=DIRECTION ( 'NONE',  ( -1.000000000000000000, 0.000000000000000000, 0.000000000000000000 ) ) ;
#13250=B_SPLINE_CURVE_WITH_KNOTS ( 'NONE', 3,
 ( #14008, #5289, #7895, #8932 ),
 .UNSPECIFIED., .F., .F.,
 ( 4, 4 ),
 ( -2.828444569873223727E-06, 0.0002461255424396390835 ),
 .UNSPECIFIED. ) ;
#13252=EDGE_CURVE ( 'NONE', #1254, #14240, #3327, .T. ) ;
#13256=DIRECTION ( 'NONE',  ( 0.000000000000000000, 1.000000000000000000, 0.000000000000000000 ) ) ;
#13257=DIRECTION ( 'NONE',  ( -0.000000000000000000, -1.000000000000000000, -0.000000000000000000 ) ) ;
#13258=ORIENTED_EDGE ( 'NONE', *, *, #10585, .T. ) ;
#13262=CARTESIAN_POINT ( 'NONE',  ( 8.148240514011916814E-17, 0.5511811023622046335, -0.6614173228346456046 ) ) ;
#13264=DIRECTION ( 'NONE',  ( -0.000000000000000000, -1.000000000000000000, -0.000000000000000000 ) ) ;
#13265=ORIENTED_EDGE ( 'NONE', *, *, #7132, .F. ) ;
#13266=VERTEX_POINT ( 'NONE', #8336 ) ;
#13285=FACE_OUTER_BOUND ( 'NONE', #14027, .T. ) ;
#13297=ORIENTED_EDGE ( 'NONE', *, *, #8852, .T. ) ;
#13298=CARTESIAN_POINT ( 'NONE',  ( 6.750021727583836750E-17, 1.622047244094488638, 0.5511811023622046335 ) ) ;
#13301=DIRECTION ( 'NONE',  ( -0.000000000000000000, -1.000000000000000000, -0.000000000000000000 ) ) ;
#13306=CARTESIAN_POINT ( 'NONE',  ( 0.000000000000000000, 0.04724409448818898960, -0.5511811023622046335 ) ) ;
#13309=ADVANCED_FACE ( 'NONE', ( #4672 ), #9461, .F. ) ;
#13316=DIRECTION ( 'NONE',  ( -0.000000000000000000, -1.000000000000000000, -0.000000000000000000 ) ) ;
#13326=AXIS2_PLACEMENT_3D ( 'NONE', #15469, #3349, #5692 ) ;
#13328=AXIS2_PLACEMENT_3D ( 'NONE', #13592, #12582, #2866 ) ;
#13335=ORIENTED_EDGE ( 'NONE', *, *, #36, .F. ) ;
#13336=ADVANCED_FACE ( 'NONE', ( #3258 ), #2071, .T. ) ;
#13338=DIRECTION ( 'NONE',  ( 0.000000000000000000, 0.000000000000000000, 1.000000000000000000 ) ) ;
#13340=CIRCLE ( 'NONE', #4079, 0.03937007874015761855 ) ;
#13341=AXIS2_PLACEMENT_3D ( 'NONE', #7762, #13798, #12550 ) ;
#13350=DIRECTION ( 'NONE',  ( 0.000000000000000000, 1.000000000000000000, 0.000000000000000000 ) ) ;
#13353=CIRCLE ( 'NONE', #8098, 0.007874015748031449116 ) ;
#13359=VERTEX_POINT ( 'NONE', #2768 ) ;
#13364=VECTOR ( 'NONE', #9370, 39.37007874015748143 ) ;
#13368=DIRECTION ( 'NONE',  ( 0.000000000000000000, 0.000000000000000000, 1.000000000000000000 ) ) ;
#13371=DIRECTION ( 'NONE',  ( 0.000000000000000000, 0.000000000000000000, -1.000000000000000000 ) ) ;
#13375=DIRECTION ( 'NONE',  ( 0.000000000000000000, 1.000000000000000000, 0.000000000000000000 ) ) ;
#13376=VERTEX_POINT ( 'NONE', #5112 ) ;
#13384=ORIENTED_EDGE ( 'NONE', *, *, #12836, .F. ) ;
#13386=DIRECTION ( 'NONE',  ( -0.000000000000000000, -1.000000000000000000, -0.000000000000000000 ) ) ;
#13389=EDGE_CURVE ( 'NONE', #6409, #11475, #5389, .T. ) ;
#13392=AXIS2_PLACEMENT_3D ( 'NONE', #7522, #7755, #327 ) ;
#13396=ORIENTED_EDGE ( 'NONE', *, *, #8162, .F. ) ;
#13398=CARTESIAN_POINT ( 'NONE',  ( -0.5905511811023621549, 2.440944881889763884, 0.000000000000000000 ) ) ;
#13400=DIRECTION ( 'NONE',  ( -0.8660254037844363761, -4.956352788505160310E-16, 0.5000000000000041078 ) ) ;
#13408=DIRECTION ( 'NONE',  ( 4.292327424963333000E-16, 1.000000000000000000, 2.478176394252540219E-16 ) ) ;
#13410=CARTESIAN_POINT ( 'NONE',  ( -0.1181102362204724809, 2.440944881889763884, 0.04724409448818898266 ) ) ;
#13413=FACE_OUTER_BOUND ( 'NONE', #5534, .T. ) ;
#13419=CARTESIAN_POINT ( 'NONE',  ( 0.000000000000000000, 0.3228346456692913757, 0.000000000000000000 ) ) ;
#13421=VERTEX_POINT ( 'NONE', #9917 ) ;
#13432=EDGE_CURVE ( 'NONE', #6371, #6490, #6639, .T. ) ;
#13434=DIRECTION ( 'NONE',  ( 1.000000000000000000, -0.000000000000000000, 1.224646799147353207E-16 ) ) ;
#13435=CARTESIAN_POINT ( 'NONE',  ( 0.000000000000000000, 1.385826771653543510, 0.000000000000000000 ) ) ;
#13439=PLANE ( 'NONE',  #4914 ) ;
#13447=DIRECTION ( 'NONE',  ( 0.000000000000000000, 0.000000000000000000, 1.000000000000000000 ) ) ;
#13450=ADVANCED_FACE ( 'NONE', ( #127 ), #3956, .T. ) ;
#13454=DIRECTION ( 'NONE',  ( -0.000000000000000000, -1.000000000000000000, -0.000000000000000000 ) ) ;
#13456=EDGE_CURVE ( 'NONE', #1832, #13926, #9767, .T. ) ;
#13457=DIRECTION ( 'NONE',  ( 0.000000000000000000, 0.000000000000000000, 1.000000000000000000 ) ) ;
#13458=FACE_OUTER_BOUND ( 'NONE', #2158, .T. ) ;
#13459=ORIENTED_EDGE ( 'NONE', *, *, #424, .F. ) ;
#13465=CIRCLE ( 'NONE', #14730, 0.1574803149606299191 ) ;
#13468=CARTESIAN_POINT ( 'NONE',  ( 0.05905511811023622659, 1.190944881889763884, -0.8267716535433072833 ) ) ;
#13472=CIRCLE ( 'NONE', #1958, 0.5590551181102362266 ) ;
#13474=ORIENTED_EDGE ( 'NONE', *, *, #5306, .F. ) ;
#13475=DIRECTION ( 'NONE',  ( -1.000000000000000000, -0.000000000000000000, -0.000000000000000000 ) ) ;
#13479=EDGE_LOOP ( 'NONE', ( #10693, #3549, #5915, #8507 ) ) ;
#13483=ORIENTED_EDGE ( 'NONE', *, *, #9029, .F. ) ;
#13489=ORIENTED_EDGE ( 'NONE', *, *, #1188, .T. ) ;
#13493=ORIENTED_EDGE ( 'NONE', *, *, #11662, .T. ) ;
#13494=ORIENTED_EDGE ( 'NONE', *, *, #13784, .F. ) ;
#13496=CARTESIAN_POINT ( 'NONE',  ( 0.1259842519685039353, 2.440944881889763884, -0.04724409448818898266 ) ) ;
#13499=PRODUCT_CONTEXT ( 'NONE', #3510, 'mechanical' ) ;
#13502=DIRECTION ( 'NONE',  ( -1.000000000000000000, 0.000000000000000000, 0.000000000000000000 ) ) ;
#13503=DIRECTION ( 'NONE',  ( 0.000000000000000000, 0.000000000000000000, -1.000000000000000000 ) ) ;
#13505=CARTESIAN_POINT ( 'NONE',  ( 7.232166136696967594E-17, 0.000000000000000000, 0.5905511811023621549 ) ) ;
#13506=ORIENTED_EDGE ( 'NONE', *, *, #6763, .T. ) ;
#13508=EDGE_CURVE ( 'NONE', #9167, #8519, #3665, .T. ) ;
#13521=LINE ( 'NONE', #8449, #2563 ) ;
#13522=CARTESIAN_POINT ( 'NONE',  ( 0.4841913566216283216, 1.338782396965247257, 0.3477389867607208473 ) ) ;
#13527=ADVANCED_FACE ( 'NONE', ( #13748 ), #10416, .T. ) ;
#13534=FACE_BOUND ( 'NONE', #6474, .T. ) ;
#13535=DIRECTION ( 'NONE',  ( 1.224646799147352961E-16, 0.000000000000000000, -1.000000000000000000 ) ) ;
#13536=DIRECTION ( 'NONE',  ( -1.224646799147352961E-16, 0.000000000000000000, -1.000000000000000000 ) ) ;
#13539=FACE_OUTER_BOUND ( 'NONE', #11290, .T. ) ;
#13541=CARTESIAN_POINT ( 'NONE',  ( 0.000000000000000000, 1.370078740157480546, 0.000000000000000000 ) ) ;
#13544=VERTEX_POINT ( 'NONE', #11235 ) ;
#13547=DIRECTION ( 'NONE',  ( -0.8660254037844432595, 0.000000000000000000, -0.4999999999999918954 ) ) ;
#13552=DIRECTION ( 'NONE',  ( 0.4999999999999920064, 0.000000000000000000, -0.8660254037844433705 ) ) ;
#13554=CARTESIAN_POINT ( 'NONE',  ( 0.4751993499420012479, 1.346456692913385877, 0.3506226965216235336 ) ) ;
#13555=CARTESIAN_POINT ( 'NONE',  ( -0.4841913566216236031, 1.338782396965247257, 0.3477389867607276752 ) ) ;
#13564=CYLINDRICAL_SURFACE ( 'NONE', #11366, 0.03937007874015751446 ) ;
#13569=ADVANCED_FACE ( 'NONE', ( #5188 ), #12647, .F. ) ;
#13571=DIRECTION ( 'NONE',  ( 0.000000000000000000, 0.000000000000000000, 1.000000000000000000 ) ) ;
#13574=ORIENTED_EDGE ( 'NONE', *, *, #8883, .F. ) ;
#13575=CIRCLE ( 'NONE', #12333, 0.5984251968503937480 ) ;
#13580=CIRCLE ( 'NONE', #3079, 0.1574803149606299191 ) ;
#13592=CARTESIAN_POINT ( 'NONE',  ( 0.000000000000000000, 2.637795275590551825, 0.03937007874015747977 ) ) ;
#13593=CARTESIAN_POINT ( 'NONE',  ( 0.000000000000000000, 1.377952755905512028, 0.5984251968503937480 ) ) ;
#13608=AXIS2_PLACEMENT_3D ( 'NONE', #12715, #1975, #4473 ) ;
#13610=TOROIDAL_SURFACE ( 'NONE', #8867, 0.5984251968503937480, 0.007874015748031495954 ) ;
#13614=DIRECTION ( 'NONE',  ( -0.000000000000000000, -1.000000000000000000, -0.000000000000000000 ) ) ;
#13619=EDGE_CURVE ( 'NONE', #6005, #14240, #7657, .T. ) ;
#13624=CIRCLE ( 'NONE', #12137, 0.5984251968503937480 ) ;
#13631=ORIENTED_EDGE ( 'NONE', *, *, #11812, .F. ) ;
#13633=UNCERTAINTY_MEASURE_WITH_UNIT (LENGTH_MEASURE( 1.000000000000000082E-05 ), #7788, 'distance_accuracy_value', 'NONE');
#13642=CARTESIAN_POINT ( 'NONE',  ( 0.000000000000000000, 0.3070866141732283561, 0.000000000000000000 ) ) ;
#13645=ADVANCED_FACE ( 'NONE', ( #12733 ), #14050, .F. ) ;
#13647=CARTESIAN_POINT ( 'NONE',  ( -0.6864776960422502849, 1.338582677165354395, 0.4645290592786118222 ) ) ;
#13648=DIRECTION ( 'NONE',  ( -0.000000000000000000, -1.000000000000000000, -0.000000000000000000 ) ) ;
#13659=CYLINDRICAL_SURFACE ( 'NONE', #4397, 0.6692913385826770867 ) ;
#13660=CARTESIAN_POINT ( 'NONE',  ( -0.6864776960422505070, 1.190944881889763884, 0.4645290592786119332 ) ) ;
#13663=TOROIDAL_SURFACE ( 'NONE', #6142, 0.1653543307086614012, 0.007874015748031495954 ) ;
#13665=VECTOR ( 'NONE', #6228, 39.37007874015748143 ) ;
#13669=DIRECTION ( 'NONE',  ( 0.000000000000000000, 0.000000000000000000, 1.000000000000000000 ) ) ;
#13679=ORIENTED_EDGE ( 'NONE', *, *, #10463, .T. ) ;
#13682=LINE ( 'NONE', #8985, #5326 ) ;
#13684=( NAMED_UNIT ( * ) SI_UNIT ( $, .STERADIAN. ) SOLID_ANGLE_UNIT ( ) );
#13685=DIRECTION ( 'NONE',  ( 0.000000000000000000, 1.000000000000000000, 0.000000000000000000 ) ) ;
#13687=LINE ( 'NONE', #5445, #11854 ) ;
#13697=ORIENTED_EDGE ( 'NONE', *, *, #10059, .T. ) ;
#13698=ORIENTED_EDGE ( 'NONE', *, *, #9797, .T. ) ;
#13708=CARTESIAN_POINT ( 'NONE',  ( 0.000000000000000000, 1.417322834645669438, -0.5590551181102362266 ) ) ;
#13713=DIRECTION ( 'NONE',  ( 0.000000000000000000, 1.000000000000000000, 0.000000000000000000 ) ) ;
#13722=LINE ( 'NONE', #2983, #8369 ) ;
#13726=DIRECTION ( 'NONE',  ( 1.224646799147343593E-16, 0.000000000000000000, -1.000000000000000000 ) ) ;
#13735=DIRECTION ( 'NONE',  ( -0.000000000000000000, -1.000000000000000000, 0.000000000000000000 ) ) ;
#13737=EDGE_CURVE ( 'NONE', #13376, #15395, #10587, .T. ) ;
#13739=EDGE_CURVE ( 'NONE', #9753, #1180, #6391, .T. ) ;
#13748=FACE_OUTER_BOUND ( 'NONE', #11711, .T. ) ;
#13752=ORIENTED_EDGE ( 'NONE', *, *, #10865, .F. ) ;
#13755=EDGE_LOOP ( 'NONE', ( #177, #3907, #13494, #1564 ) ) ;
#13767=EDGE_LOOP ( 'NONE', ( #11961, #15241, #9401, #9582 ) ) ;
#13772=CARTESIAN_POINT ( 'NONE',  ( 0.000000000000000000, 1.661417322834646049, -0.5905511811023621549 ) ) ;
#13780=CARTESIAN_POINT ( 'NONE',  ( 0.000000000000000000, 0.007874015748031480341, -0.1574803149606299191 ) ) ;
#13784=EDGE_CURVE ( 'NONE', #10400, #1599, #673, .T. ) ;
#13785=LINE ( 'NONE', #12536, #4855 ) ;
#13790=CARTESIAN_POINT ( 'NONE',  ( 0.000000000000000000, 0.5590551181102362266, 0.000000000000000000 ) ) ;
#13791=CARTESIAN_POINT ( 'NONE',  ( 0.000000000000000000, -1.707404996040164512E-17, 0.5826771653543306728 ) ) ;
#13794=DIRECTION ( 'NONE',  ( 0.000000000000000000, 1.000000000000000000, 0.000000000000000000 ) ) ;
#13798=DIRECTION ( 'NONE',  ( -0.4999999999999919509, 0.000000000000000000, 0.8660254037844432595 ) ) ;
#13805=CARTESIAN_POINT ( 'NONE',  ( 0.000000000000000000, 0.007874015748031480341, 0.1653543307086614012 ) ) ;
#13806=FACE_OUTER_BOUND ( 'NONE', #12860, .T. ) ;
#13808=FACE_OUTER_BOUND ( 'NONE', #3507, .T. ) ;
#13810=DIRECTION ( 'NONE',  ( 0.000000000000000000, 0.000000000000000000, 1.000000000000000000 ) ) ;
#13815=EDGE_CURVE ( 'NONE', #9431, #11475, #1658, .T. ) ;
#13832=ORIENTED_EDGE ( 'NONE', *, *, #14480, .T. ) ;
#13833=AXIS2_PLACEMENT_3D ( 'NONE', #1478, #14719, #3980 ) ;
#13837=ORIENTED_EDGE ( 'NONE', *, *, #3960, .T. ) ;
#13847=CARTESIAN_POINT ( 'NONE',  ( 0.000000000000000000, 1.645669291338583085, -0.7007874015748031260 ) ) ;
#13849=AXIS2_PLACEMENT_3D ( 'NONE', #575, #9042, #5336 ) ;
#13852=ORIENTED_EDGE ( 'NONE', *, *, #7891, .T. ) ;
#13854=DIRECTION ( 'NONE',  ( -0.000000000000000000, -1.000000000000000000, -0.000000000000000000 ) ) ;
#13857=TOROIDAL_SURFACE ( 'NONE', #355, 0.5590551181102362266, 0.007874015748031495954 ) ;
#13862=VECTOR ( 'NONE', #4865, 39.37007874015748143 ) ;
#13873=AXIS2_PLACEMENT_3D ( 'NONE', #783, #6796, #15277 ) ;
#13874=DIRECTION ( 'NONE',  ( 0.000000000000000000, 0.000000000000000000, 1.000000000000000000 ) ) ;
#13878=ORIENTED_EDGE ( 'NONE', *, *, #1408, .F. ) ;
#13883=CIRCLE ( 'NONE', #3875, 0.007874015748031516770 ) ;
#13886=CARTESIAN_POINT ( 'NONE',  ( -0.1181102362204724254, 2.448818897637795367, -0.03937007874015747977 ) ) ;
#13887=FACE_OUTER_BOUND ( 'NONE', #10696, .T. ) ;
#13889=CYLINDRICAL_SURFACE ( 'NONE', #1201, 0.5511811023622046335 ) ;
#13890=LINE ( 'NONE', #4411, #5115 ) ;
#13893=EDGE_CURVE ( 'NONE', #1166, #14956, #4168, .T. ) ;
#13896=CIRCLE ( 'NONE', #7139, 0.7007874015748031260 ) ;
#13900=AXIS2_PLACEMENT_3D ( 'NONE', #4282, #6482, #8933 ) ;
#13902=DIRECTION ( 'NONE',  ( 0.000000000000000000, 0.000000000000000000, -1.000000000000000000 ) ) ;
#13904=ORIENTED_EDGE ( 'NONE', *, *, #8976, .F. ) ;
#13908=ADVANCED_FACE ( 'NONE', ( #8632, #13413 ), #2682, .F. ) ;
#13909=AXIS2_PLACEMENT_3D ( 'NONE', #1362, #14528, #3789 ) ;
#13917=DIRECTION ( 'NONE',  ( 0.000000000000000000, 0.000000000000000000, -1.000000000000000000 ) ) ;
#13918=DIRECTION ( 'NONE',  ( -1.000000000000000000, -0.000000000000000000, -0.000000000000000000 ) ) ;
#13919=CARTESIAN_POINT ( 'NONE',  ( 0.000000000000000000, 0.3149606299212598381, 0.000000000000000000 ) ) ;
#13921=AXIS2_PLACEMENT_3D ( 'NONE', #2941, #15008, #1994 ) ;
#13923=ORIENTED_EDGE ( 'NONE', *, *, #9361, .F. ) ;
#13926=VERTEX_POINT ( 'NONE', #13647 ) ;
#13928=EDGE_CURVE ( 'NONE', #10377, #7046, #4415, .T. ) ;
#13929=CARTESIAN_POINT ( 'NONE',  ( 8.100026073100603114E-17, 1.606299212598425674, -0.6614173228346456046 ) ) ;
#13932=DIRECTION ( 'NONE',  ( -0.000000000000000000, -1.000000000000000000, -0.000000000000000000 ) ) ;
#13940=DIRECTION ( 'NONE',  ( 0.000000000000000000, 0.000000000000000000, 1.000000000000000000 ) ) ;
#13944=AXIS2_PLACEMENT_3D ( 'NONE', #6784, #14966, #8934 ) ;
#13947=LINE ( 'NONE', #6645, #5354 ) ;
#13950=CARTESIAN_POINT ( 'NONE',  ( 0.000000000000000000, 0.000000000000000000, -0.5511811023622046335 ) ) ;
#13951=EDGE_CURVE ( 'NONE', #13266, #12883, #14435, .T. ) ;
#13953=TOROIDAL_SURFACE ( 'NONE', #7199, 0.1653543307086614012, 0.007874015748031495954 ) ;
#13955=ORIENTED_EDGE ( 'NONE', *, *, #11796, .F. ) ;
#13969=CARTESIAN_POINT ( 'NONE',  ( 0.000000000000000000, -1.707404996040164512E-17, 0.1653543307086614012 ) ) ;
#13981=AXIS2_PLACEMENT_3D ( 'NONE', #4056, #14801, #14563 ) ;
#13997=CYLINDRICAL_SURFACE ( 'NONE', #5652, 0.007874015748031482076 ) ;
#13998=EDGE_CURVE ( 'NONE', #2247, #692, #727, .T. ) ;
#14003=ADVANCED_FACE ( 'NONE', ( #4074 ), #10117, .T. ) ;
#14008=CARTESIAN_POINT ( 'NONE',  ( 0.4751993499420012479, 1.346456692913385877, 0.3506226965216235336 ) ) ;
#14024=DIRECTION ( 'NONE',  ( 0.000000000000000000, 0.000000000000000000, -1.000000000000000000 ) ) ;
#14025=CARTESIAN_POINT ( 'NONE',  ( 0.000000000000000000, 0.000000000000000000, 0.000000000000000000 ) ) ;
#14027=EDGE_LOOP ( 'NONE', ( #1219, #1057 ) ) ;
#14028=CARTESIAN_POINT ( 'NONE',  ( 0.5405850968741658935, 1.037100910086334205, 0.2377418676364856376 ) ) ;
#14030=CARTESIAN_POINT ( 'NONE',  ( -0.4765556591342228199, 1.037732670558789483, 0.3487844890899370887 ) ) ;
#14031=EDGE_CURVE ( 'NONE', #5195, #7046, #1806, .T. ) ;
#14038=ORIENTED_EDGE ( 'NONE', *, *, #5519, .T. ) ;
#14040=ORIENTED_EDGE ( 'NONE', *, *, #2551, .F. ) ;
#14041=CARTESIAN_POINT ( 'NONE',  ( 0.000000000000000000, 0.007874015748031480341, 0.000000000000000000 ) ) ;
#14043=EDGE_CURVE ( 'NONE', #15234, #5486, #12776, .T. ) ;
#14044=DIRECTION ( 'NONE',  ( -0.000000000000000000, -1.000000000000000000, -0.000000000000000000 ) ) ;
#14049=VERTEX_POINT ( 'NONE', #6734 ) ;
#14050=CYLINDRICAL_SURFACE ( 'NONE', #9930, 0.007874015748031499423 ) ;
#14058=EDGE_LOOP ( 'NONE', ( #8554, #2982 ) ) ;
#14063=FACE_OUTER_BOUND ( 'NONE', #11655, .T. ) ;
#14064=DIRECTION ( 'NONE',  ( -0.5000000000000039968, 0.000000000000000000, -0.8660254037844362651 ) ) ;
#14079=EDGE_LOOP ( 'NONE', ( #12722, #2771, #15347, #11182 ) ) ;
#14092=EDGE_CURVE ( 'NONE', #1546, #1436, #1671, .T. ) ;
#14093=CIRCLE ( 'NONE', #12338, 0.007874015748031516770 ) ;
#14101=EDGE_CURVE ( 'NONE', #7333, #3058, #7083, .T. ) ;
#14116=TOROIDAL_SURFACE ( 'NONE', #2103, 0.6614173228346456046, 0.007874015748031495954 ) ;
#14131=FACE_OUTER_BOUND ( 'NONE', #5521, .T. ) ;
#14133=ORIENTED_EDGE ( 'NONE', *, *, #4945, .T. ) ;
#14139=CARTESIAN_POINT ( 'NONE',  ( 0.5445274672588121812, 1.043263280880422528, 0.2461921031270739857 ) ) ;
#14140=ORIENTED_EDGE ( 'NONE', *, *, #1581, .F. ) ;
#14141=CIRCLE ( 'NONE', #872, 0.5511811023622046335 ) ;
#14143=VERTEX_POINT ( 'NONE', #2272 ) ;
#14144=DIRECTION ( 'NONE',  ( 0.000000000000000000, 0.000000000000000000, 1.000000000000000000 ) ) ;
#14155=DIRECTION ( 'NONE',  ( 0.000000000000000000, 0.000000000000000000, -1.000000000000000000 ) ) ;
#14163=CIRCLE ( 'NONE', #9673, 0.5984251968503937480 ) ;
#14182=PLANE ( 'NONE',  #7611 ) ;
#14184=CARTESIAN_POINT ( 'NONE',  ( -0.7455328141524873997, 1.190944881889763884, 0.3622425942647021779 ) ) ;
#14187=CYLINDRICAL_SURFACE ( 'NONE', #10476, 0.007874015748031499423 ) ;
#14202=VERTEX_POINT ( 'NONE', #6016 ) ;
#14203=EDGE_CURVE ( 'NONE', #6519, #2233, #10179, .T. ) ;
#14204=DIRECTION ( 'NONE',  ( -0.000000000000000000, -1.000000000000000000, -0.000000000000000000 ) ) ;
#14205=LINE ( 'NONE', #10442, #655 ) ;
#14210=CIRCLE ( 'NONE', #7443, 0.5511811023622046335 ) ;
#14217=DIRECTION ( 'NONE',  ( 0.000000000000000000, 0.000000000000000000, -1.000000000000000000 ) ) ;
#14218=AXIS2_PLACEMENT_3D ( 'NONE', #14443, #15080, #11643 ) ;
#14223=ORIENTED_EDGE ( 'NONE', *, *, #3755, .T. ) ;
#14224=VECTOR ( 'NONE', #11218, 39.37007874015748143 ) ;
#14233=AXIS2_PLACEMENT_3D ( 'NONE', #1433, #7521, #9810 ) ;
#14239=EDGE_LOOP ( 'NONE', ( #9097, #5932, #9262, #9170 ) ) ;
#14240=VERTEX_POINT ( 'NONE', #13306 ) ;
#14243=ADVANCED_FACE ( 'NONE', ( #14566 ), #10023, .F. ) ;
#14249=DIRECTION ( 'NONE',  ( -1.000000000000000000, 0.000000000000000000, 0.000000000000000000 ) ) ;
#14251=CARTESIAN_POINT ( 'NONE',  ( 0.000000000000000000, -1.707404996040164512E-17, 0.000000000000000000 ) ) ;
#14261=DIRECTION ( 'NONE',  ( 1.224646799147343593E-16, 0.000000000000000000, -1.000000000000000000 ) ) ;
#14265=EDGE_LOOP ( 'NONE', ( #328, #10342, #2052, #9282, #10150, #7402, #7346 ) ) ;
#14274=FACE_OUTER_BOUND ( 'NONE', #337, .T. ) ;
#14280=ADVANCED_FACE ( 'NONE', ( #13539 ), #2801, .F. ) ;
#14282=ORIENTED_EDGE ( 'NONE', *, *, #11953, .T. ) ;
#14283=CARTESIAN_POINT ( 'NONE',  ( -0.1181102362204723977, 2.444206406002937815, 0.03937007874015747977 ) ) ;
#14290=ORIENTED_EDGE ( 'NONE', *, *, #14704, .F. ) ;
#14299=EDGE_CURVE ( 'NONE', #14592, #697, #5066, .T. ) ;
#14303=EDGE_CURVE ( 'NONE', #1695, #11091, #4438, .T. ) ;
#14305=FACE_OUTER_BOUND ( 'NONE', #14748, .T. ) ;
#14307=EDGE_LOOP ( 'NONE', ( #8792, #3788, #68, #5755 ) ) ;
#14315=DIRECTION ( 'NONE',  ( -0.000000000000000000, -0.000000000000000000, -1.000000000000000000 ) ) ;
#14326=DIRECTION ( 'NONE',  ( -0.8660254037844363761, -4.956352788505160310E-16, 0.5000000000000041078 ) ) ;
#14332=DIRECTION ( 'NONE',  ( 1.000000000000000000, 0.000000000000000000, 0.000000000000000000 ) ) ;
#14336=CARTESIAN_POINT ( 'NONE',  ( -0.06278592661683286835, 1.343094183513035222, -0.5877247716201634553 ) ) ;
#14338=CARTESIAN_POINT ( 'NONE',  ( 0.5445274672588121812, 1.338626482899105241, 0.2461921031270739857 ) ) ;
#14340=VECTOR ( 'NONE', #3002, 39.37007874015748143 ) ;
#14343=CIRCLE ( 'NONE', #4083, 0.5905511811023621549 ) ;
#14344=ORIENTED_EDGE ( 'NONE', *, *, #10213, .T. ) ;
#14348=CARTESIAN_POINT ( 'NONE',  ( 0.1181102362204724254, 2.448818897637795367, -0.03937007874015747977 ) ) ;
#14351=CARTESIAN_POINT ( 'NONE',  ( 0.000000000000000000, 1.606299212598425674, 0.000000000000000000 ) ) ;
#14360=VERTEX_POINT ( 'NONE', #12763 ) ;
#14363=ORIENTED_EDGE ( 'NONE', *, *, #12836, .T. ) ;
#14384=CARTESIAN_POINT ( 'NONE',  ( 0.000000000000000000, 0.007874015748031480341, 0.000000000000000000 ) ) ;
#14393=AXIS2_PLACEMENT_3D ( 'NONE', #8731, #12327, #4179 ) ;
#14415=DIRECTION ( 'NONE',  ( 0.000000000000000000, 1.000000000000000000, 0.000000000000000000 ) ) ;
#14422=CARTESIAN_POINT ( 'NONE',  ( 0.000000000000000000, 0.3622047244094487306, -0.6692913385826770867 ) ) ;
#14427=VERTEX_POINT ( 'NONE', #3276 ) ;
#14428=DIRECTION ( 'NONE',  ( -1.000000000000000000, 0.000000000000000000, 0.000000000000000000 ) ) ;
#14429=PLANE ( 'NONE',  #3360 ) ;
#14432=ORIENTED_EDGE ( 'NONE', *, *, #11371, .F. ) ;
#14435=CIRCLE ( 'NONE', #3436, 0.5590551181102362266 ) ;
#14443=CARTESIAN_POINT ( 'NONE',  ( 0.1181102362204724254, 2.440944881889764329, 0.03937007874015747977 ) ) ;
#14447=CARTESIAN_POINT ( 'NONE',  ( 0.000000000000000000, 1.385826771653543510, 0.7007874015748031260 ) ) ;
#14449=FACE_OUTER_BOUND ( 'NONE', #9022, .T. ) ;
#14450=VECTOR ( 'NONE', #9011, 39.37007874015748143 ) ;
#14454=VERTEX_POINT ( 'NONE', #9162 ) ;
#14458=DIRECTION ( 'NONE',  ( 0.000000000000000000, 0.000000000000000000, 1.000000000000000000 ) ) ;
#14463=AXIS2_PLACEMENT_3D ( 'NONE', #15465, #1130, #3309 ) ;
#14466=DIRECTION ( 'NONE',  ( 0.000000000000000000, 0.000000000000000000, -1.000000000000000000 ) ) ;
#14473=ORIENTED_EDGE ( 'NONE', *, *, #1800, .F. ) ;
#14474=ORIENTED_EDGE ( 'NONE', *, *, #752, .T. ) ;
#14475=ORIENTED_EDGE ( 'NONE', *, *, #10676, .T. ) ;
#14480=EDGE_CURVE ( 'NONE', #7594, #14202, #11507, .T. ) ;
#14482=DIRECTION ( 'NONE',  ( -1.000000000000000000, -4.292327424963298981E-16, 5.289613918361266480E-33 ) ) ;
#14490=ORIENTED_EDGE ( 'NONE', *, *, #8636, .T. ) ;
#14495=CARTESIAN_POINT ( 'NONE',  ( -0.5424653753748054363, 1.043012296488531332, 0.2450015538227584277 ) ) ;
#14496=ADVANCED_FACE ( 'NONE', ( #10318 ), #5423, .T. ) ;
#14504=ORIENTED_EDGE ( 'NONE', *, *, #15420, .T. ) ;
#14507=EDGE_LOOP ( 'NONE', ( #9469, #2710 ) ) ;
#14528=DIRECTION ( 'NONE',  ( 0.000000000000000000, 1.000000000000000000, 0.000000000000000000 ) ) ;
#14530=CARTESIAN_POINT ( 'NONE',  ( 0.000000000000000000, 1.417322834645669438, 0.000000000000000000 ) ) ;
#14533=DIRECTION ( 'NONE',  ( 0.000000000000000000, 1.000000000000000000, 0.000000000000000000 ) ) ;
#14535=DIRECTION ( 'NONE',  ( 0.000000000000000000, 0.000000000000000000, -1.000000000000000000 ) ) ;
#14537=DIRECTION ( 'NONE',  ( 1.000000000000000000, 0.000000000000000000, 0.000000000000000000 ) ) ;
#14539=ORIENTED_EDGE ( 'NONE', *, *, #2774, .T. ) ;
#14543=CARTESIAN_POINT ( 'NONE',  ( -0.6864776960422502849, 1.338582677165354395, 0.4645290592786118222 ) ) ;
#14548=DIRECTION ( 'NONE',  ( 0.000000000000000000, 0.000000000000000000, -1.000000000000000000 ) ) ;
#14549=CARTESIAN_POINT ( 'NONE',  ( 0.000000000000000000, 1.622047244094488638, 0.000000000000000000 ) ) ;
#14550=CARTESIAN_POINT ( 'NONE',  ( 0.000000000000000000, 0.03937007874015749365, 0.000000000000000000 ) ) ;
#14553=ORIENTED_EDGE ( 'NONE', *, *, #8883, .T. ) ;
#14554=B_SPLINE_CURVE_WITH_KNOTS ( 'NONE', 3,
 ( #15128, #12850, #2208, #7997 ),
 .UNSPECIFIED., .F., .F.,
 ( 4, 4 ),
 ( 0.000000000000000000, 2.119993237936781635E-05 ),
 .UNSPECIFIED. ) ;
#14559=ADVANCED_FACE ( 'NONE', ( #10789 ), #3936, .F. ) ;
#14561=DIRECTION ( 'NONE',  ( -1.224646799147353947E-16, 0.000000000000000000, -1.000000000000000000 ) ) ;
#14563=DIRECTION ( 'NONE',  ( 0.000000000000000000, 0.000000000000000000, 1.000000000000000000 ) ) ;
#14566=FACE_OUTER_BOUND ( 'NONE', #3050, .T. ) ;
#14567=DIRECTION ( 'NONE',  ( -0.000000000000000000, 0.000000000000000000, -1.000000000000000000 ) ) ;
#14569=VERTEX_POINT ( 'NONE', #13145 ) ;
#14577=CARTESIAN_POINT ( 'NONE',  ( 0.4815353412745612127, 0.000000000000000000, 0.3552976658085785222 ) ) ;
#14578=DIRECTION ( 'NONE',  ( -0.000000000000000000, -1.000000000000000000, -0.000000000000000000 ) ) ;
#14584=AXIS2_PLACEMENT_3D ( 'NONE', #11987, #1246, #5998 ) ;
#14590=ADVANCED_FACE ( 'NONE', ( #4763 ), #5928, .F. ) ;
#14592=VERTEX_POINT ( 'NONE', #15429 ) ;
#14593=EDGE_CURVE ( 'NONE', #6490, #6371, #3190, .T. ) ;
#14595=DIRECTION ( 'NONE',  ( 0.000000000000000000, 0.000000000000000000, -1.000000000000000000 ) ) ;
#14597=VECTOR ( 'NONE', #4860, 39.37007874015748143 ) ;
#14603=AXIS2_PLACEMENT_3D ( 'NONE', #6566, #14908, #15212 ) ;
#14606=DIRECTION ( 'NONE',  ( -0.000000000000000000, -1.000000000000000000, -0.000000000000000000 ) ) ;
#14623=EDGE_CURVE ( 'NONE', #3165, #8556, #11205, .T. ) ;
#14625=TOROIDAL_SURFACE ( 'NONE', #8113, 0.1653543307086614012, 0.007874015748031495954 ) ;
#14636=ADVANCED_FACE ( 'NONE', ( #7553 ), #5182, .T. ) ;
#14637=DIRECTION ( 'NONE',  ( -0.000000000000000000, -0.000000000000000000, -1.000000000000000000 ) ) ;
#14638=CARTESIAN_POINT ( 'NONE',  ( 0.6864776960422569463, 1.190944881889763884, 0.4645290592786023298 ) ) ;
#14643=AXIS2_PLACEMENT_3D ( 'NONE', #9577, #6258, #8408 ) ;
#14644=AXIS2_PLACEMENT_3D ( 'NONE', #3283, #15275, #5472 ) ;
#14647=AXIS2_PLACEMENT_3D ( 'NONE', #4704, #9492, #14261 ) ;
#14651=FACE_OUTER_BOUND ( 'NONE', #13133, .T. ) ;
#14656=AXIS2_PLACEMENT_3D ( 'NONE', #5374, #13386, #3909 ) ;
#14657=ORIENTED_EDGE ( 'NONE', *, *, #10564, .T. ) ;
#14659=CARTESIAN_POINT ( 'NONE',  ( 0.000000000000000000, 1.035433070866142113, 0.000000000000000000 ) ) ;
#14660=VECTOR ( 'NONE', #5461, 39.37007874015748854 ) ;
#14662=ORIENTED_EDGE ( 'NONE', *, *, #5013, .F. ) ;
#14664=CIRCLE ( 'NONE', #3900, 0.6692913385826770867 ) ;
#14665=EDGE_LOOP ( 'NONE', ( #9800, #3567, #3504, #903 ) ) ;
#14667=AXIS2_PLACEMENT_3D ( 'NONE', #3159, #2927, #7703 ) ;
#14670=CARTESIAN_POINT ( 'NONE',  ( 1.928577636452524610E-17, 0.000000000000000000, 0.1574803149606299191 ) ) ;
#14673=DIRECTION ( 'NONE',  ( -0.000000000000000000, 1.000000000000000000, -0.000000000000000000 ) ) ;
#14676=DIRECTION ( 'NONE',  ( 0.000000000000000000, 0.000000000000000000, -1.000000000000000000 ) ) ;
#14678=CARTESIAN_POINT ( 'NONE',  ( 2.025006518275150778E-17, 0.03149606299212599769, 0.1653543307086614012 ) ) ;
#14687=VERTEX_POINT ( 'NONE', #12437 ) ;
#14695=DIRECTION ( 'NONE',  ( 0.000000000000000000, 0.000000000000000000, -1.000000000000000000 ) ) ;
#14698=DIRECTION ( 'NONE',  ( 0.000000000000000000, 0.000000000000000000, -1.000000000000000000 ) ) ;
#14699=ADVANCED_FACE ( 'NONE', ( #6466 ), #5570, .F. ) ;
#14704=EDGE_CURVE ( 'NONE', #9168, #15219, #6944, .T. ) ;
#14706=ADVANCED_FACE ( 'NONE', ( #7066 ), #4654, .T. ) ;
#14707=ORIENTED_EDGE ( 'NONE', *, *, #3413, .T. ) ;
#14710=DIRECTION ( 'NONE',  ( 8.673617379884028076E-17, 1.000000000000000000, 0.000000000000000000 ) ) ;
#14712=CARTESIAN_POINT ( 'NONE',  ( 0.000000000000000000, 2.637795275590551825, -0.03937007874015747977 ) ) ;
#14719=DIRECTION ( 'NONE',  ( -0.000000000000000000, -1.000000000000000000, -0.000000000000000000 ) ) ;
#14720=CARTESIAN_POINT ( 'NONE',  ( 0.000000000000000000, 0.3464566929133857109, 0.000000000000000000 ) ) ;
#14721=ORIENTED_EDGE ( 'NONE', *, *, #14203, .T. ) ;
#14724=EDGE_CURVE ( 'NONE', #2195, #1428, #7692, .T. ) ;
#14730=AXIS2_PLACEMENT_3D ( 'NONE', #547, #3999, #6313 ) ;
#14738=CARTESIAN_POINT ( 'NONE',  ( 0.05905511811023621271, 1.043012296488531332, -0.5922895726594219479 ) ) ;
#14741=ORIENTED_EDGE ( 'NONE', *, *, #7483, .F. ) ;
#14746=VERTEX_POINT ( 'NONE', #9276 ) ;
#14748=EDGE_LOOP ( 'NONE', ( #2297, #5699, #8919, #14865 ) ) ;
#14749=EDGE_CURVE ( 'NONE', #8826, #12461, #5891, .T. ) ;
#14750=CARTESIAN_POINT ( 'NONE',  ( 0.000000000000000000, 1.409448818897637956, 0.000000000000000000 ) ) ;
#14777=ADVANCED_FACE ( 'NONE', ( #1216, #14131 ), #4416, .F. ) ;
#14778=DIRECTION ( 'NONE',  ( -0.000000000000000000, -1.000000000000000000, -0.000000000000000000 ) ) ;
#14780=LINE ( 'NONE', #6525, #956 ) ;
#14792=EDGE_CURVE ( 'NONE', #7799, #6857, #1511, .T. ) ;
#14801=DIRECTION ( 'NONE',  ( -1.000000000000000000, 0.000000000000000000, 0.000000000000000000 ) ) ;
#14804=DIRECTION ( 'NONE',  ( -0.000000000000000000, -1.000000000000000000, -0.000000000000000000 ) ) ;
#14808=ORIENTED_EDGE ( 'NONE', *, *, #13951, .F. ) ;
#14811=DIRECTION ( 'NONE',  ( 0.000000000000000000, 0.000000000000000000, -1.000000000000000000 ) ) ;
#14819=DIRECTION ( 'NONE',  ( 0.000000000000000000, 1.000000000000000000, 0.000000000000000000 ) ) ;
#14822=CARTESIAN_POINT ( 'NONE',  ( -0.5452492930724200937, 1.043307086614173373, 0.2466088494548779875 ) ) ;
#14823=EDGE_CURVE ( 'NONE', #563, #10886, #15466, .T. ) ;
#14834=LINE ( 'NONE', #6356, #10632 ) ;
#14836=DIRECTION ( 'NONE',  ( 0.000000000000000000, 1.000000000000000000, 0.000000000000000000 ) ) ;
#14842=ORIENTED_EDGE ( 'NONE', *, *, #4532, .T. ) ;
#14845=VECTOR ( 'NONE', #13080, 39.37007874015748854 ) ;
#14849=( NAMED_UNIT ( * ) PLANE_ANGLE_UNIT ( ) SI_UNIT ( $, .RADIAN. ) );
#14856=EDGE_CURVE ( 'NONE', #14240, #6005, #14210, .T. ) ;
#14857=VECTOR ( 'NONE', #6982, 39.37007874015748143 ) ;
#14858=DIRECTION ( 'NONE',  ( -0.000000000000000000, -1.000000000000000000, -0.000000000000000000 ) ) ;
#14863=ORIENTED_EDGE ( 'NONE', *, *, #13893, .T. ) ;
#14865=ORIENTED_EDGE ( 'NONE', *, *, #10364, .F. ) ;
#14866=EDGE_CURVE ( 'NONE', #15338, #12857, #8215, .T. ) ;
#14868=VECTOR ( 'NONE', #3650, 39.37007874015748854 ) ;
#14879=CARTESIAN_POINT ( 'NONE',  ( -0.4854723491485721798, 1.338626482899105241, 0.3484785681409913738 ) ) ;
#14880=DIRECTION ( 'NONE',  ( 0.000000000000000000, 0.000000000000000000, -1.000000000000000000 ) ) ;
#14883=ORIENTED_EDGE ( 'NONE', *, *, #6646, .T. ) ;
#14886=CARTESIAN_POINT ( 'NONE',  ( 0.000000000000000000, 1.606299212598425674, 0.000000000000000000 ) ) ;
#14887=AXIS2_PLACEMENT_3D ( 'NONE', #11063, #350, #14695 ) ;
#14890=EDGE_CURVE ( 'NONE', #11226, #12382, #10446, .T. ) ;
#14891=CIRCLE ( 'NONE', #7875, 0.5984251968503937480 ) ;
#14893=ORIENTED_EDGE ( 'NONE', *, *, #11548, .F. ) ;
#14897=ORIENTED_EDGE ( 'NONE', *, *, #13784, .T. ) ;
#14903=CYLINDRICAL_SURFACE ( 'NONE', #13127, 0.7086614173228346081 ) ;
#14906=ORIENTED_EDGE ( 'NONE', *, *, #529, .F. ) ;
#14908=DIRECTION ( 'NONE',  ( -0.000000000000000000, -1.000000000000000000, -0.000000000000000000 ) ) ;
#14916=EDGE_CURVE ( 'NONE', #5785, #6404, #12398, .T. ) ;
#14920=LINE ( 'NONE', #9034, #4151 ) ;
#14926=CARTESIAN_POINT ( 'NONE',  ( 6.701807286672523049E-17, 2.401574803149606918, -0.5433070866141731514 ) ) ;
#14928=DIRECTION ( 'NONE',  ( 0.000000000000000000, 0.000000000000000000, -1.000000000000000000 ) ) ;
#14942=LENGTH_MEASURE_WITH_UNIT ( LENGTH_MEASURE( 0.02539999999999999897 ), #5512 );
#14955=ORIENTED_EDGE ( 'NONE', *, *, #12193, .T. ) ;
#14956=VERTEX_POINT ( 'NONE', #9095 ) ;
#14957=CIRCLE ( 'NONE', #10940, 0.5905511811023621549 ) ;
#14958=CARTESIAN_POINT ( 'NONE',  ( 0.4854723491485768982, 1.338626482899105241, 0.3484785681409844904 ) ) ;
#14962=EDGE_CURVE ( 'NONE', #9379, #8620, #9976, .T. ) ;
#14966=DIRECTION ( 'NONE',  ( -0.000000000000000000, -1.000000000000000000, -0.000000000000000000 ) ) ;
#14968=ORIENTED_EDGE ( 'NONE', *, *, #12614, .T. ) ;
#14972=TOROIDAL_SURFACE ( 'NONE', #4445, 0.6614173228346456046, 0.007874015748031495954 ) ;
#14973=ORIENTED_EDGE ( 'NONE', *, *, #6234, .F. ) ;
#14976=ORIENTED_EDGE ( 'NONE', *, *, #12193, .F. ) ;
#14980=CARTESIAN_POINT ( 'NONE',  ( -0.4815353412745217998, 1.041793866378536437, 0.3474236500605538125 ) ) ;
#14986=EDGE_CURVE ( 'NONE', #5486, #12971, #14554, .T. ) ;
#14987=DIRECTION ( 'NONE',  ( 0.000000000000000000, 0.000000000000000000, -1.000000000000000000 ) ) ;
#14990=ORIENTED_EDGE ( 'NONE', *, *, #10303, .F. ) ;
#14995=DIRECTION ( 'NONE',  ( -1.000000000000000000, -0.000000000000000000, -0.000000000000000000 ) ) ;
#14996=CARTESIAN_POINT ( 'NONE',  ( -0.7114373258145173518, 1.190944881889763884, 0.3425575548946232507 ) ) ;
#15008=DIRECTION ( 'NONE',  ( 0.000000000000000000, 1.000000000000000000, 0.000000000000000000 ) ) ;
#15011=EDGE_CURVE ( 'NONE', #8722, #1546, #11766, .T. ) ;
#15018=CARTESIAN_POINT ( 'NONE',  ( 0.4815353412745266848, 1.041793866378536437, 0.3474236500605469291 ) ) ;
#15022=CARTESIAN_POINT ( 'NONE',  ( 0.000000000000000000, 0.5590551181102362266, 0.000000000000000000 ) ) ;
#15023=ORIENTED_EDGE ( 'NONE', *, *, #13928, .F. ) ;
#15029=DIRECTION ( 'NONE',  ( 0.000000000000000000, 0.000000000000000000, -1.000000000000000000 ) ) ;
#15031=CARTESIAN_POINT ( 'NONE',  ( 0.05905511811023622659, 1.338582677165354395, -0.5952259495879738127 ) ) ;
#15033=CARTESIAN_POINT ( 'NONE',  ( 0.000000000000000000, -1.707404996040164512E-17, 0.000000000000000000 ) ) ;
#15039=EDGE_LOOP ( 'NONE', ( #14474, #5508, #6040, #11129 ) ) ;
#15043=EDGE_CURVE ( 'NONE', #12332, #14746, #15214, .T. ) ;
#15049=FACE_OUTER_BOUND ( 'NONE', #8168, .T. ) ;
#15062=DIRECTION ( 'NONE',  ( 0.000000000000000000, 0.000000000000000000, -1.000000000000000000 ) ) ;
#15065=ORIENTED_EDGE ( 'NONE', *, *, #11168, .F. ) ;
#15067=CARTESIAN_POINT ( 'NONE',  ( 0.000000000000000000, 0.03937007874015749365, -0.5433070866141731514 ) ) ;
#15069=CARTESIAN_POINT ( 'NONE',  ( 0.000000000000000000, 0.007874015748031480341, -0.5905511811023621549 ) ) ;
#15075=EDGE_LOOP ( 'NONE', ( #8571, #5121, #10792, #3249 ) ) ;
#15078=CARTESIAN_POINT ( 'NONE',  ( 0.5445274672588121812, 1.043263280880422528, 0.2461921031270739857 ) ) ;
#15080=DIRECTION ( 'NONE',  ( -1.000000000000000000, 8.673617379884029309E-17, 0.000000000000000000 ) ) ;
#15085=EDGE_LOOP ( 'NONE', ( #8432, #9117, #5886, #8417 ) ) ;
#15087=ORIENTED_EDGE ( 'NONE', *, *, #4046, .T. ) ;
#15094=TOROIDAL_SURFACE ( 'NONE', #10325, 0.5590551181102362266, 0.007874015748031495954 ) ;
#15097=CARTESIAN_POINT ( 'NONE',  ( 0.000000000000000000, 0.3228346456692913757, 0.000000000000000000 ) ) ;
#15101=TOROIDAL_SURFACE ( 'NONE', #7839, 0.5984251968503937480, 0.007874015748031495954 ) ;
#15105=DIRECTION ( 'NONE',  ( 0.5000000000000041078, -0.000000000000000000, 0.8660254037844363761 ) ) ;
#15107=ORIENTED_EDGE ( 'NONE', *, *, #4515, .F. ) ;
#15109=AXIS2_PLACEMENT_3D ( 'NONE', #10714, #4111, #12339 ) ;
#15118=CYLINDRICAL_SURFACE ( 'NONE', #5452, 0.5511811023622046335 ) ;
#15119=VECTOR ( 'NONE', #12655, 39.37007874015748854 ) ;
#15122=VECTOR ( 'NONE', #14326, 39.37007874015747433 ) ;
#15123=ORIENTED_EDGE ( 'NONE', *, *, #14856, .F. ) ;
#15125=AXIS2_PLACEMENT_3D ( 'NONE', #15205, #1887, #6648 ) ;
#15128=CARTESIAN_POINT ( 'NONE',  ( -0.05905511811023622659, 1.338626482899105241, -0.5946706712680680518 ) ) ;
#15137=ORIENTED_EDGE ( 'NONE', *, *, #11056, .T. ) ;
#15141=CIRCLE ( 'NONE', #883, 0.5590551181102362266 ) ;
#15142=EDGE_CURVE ( 'NONE', #12889, #3736, #11468, .T. ) ;
#15160=ORIENTED_EDGE ( 'NONE', *, *, #702, .T. ) ;
#15166=ADVANCED_FACE ( 'NONE', ( #11931, #10970 ), #3765, .T. ) ;
#15168=DIRECTION ( 'NONE',  ( 1.000000000000000000, -0.000000000000000000, 1.224646799147353207E-16 ) ) ;
#15171=DIRECTION ( 'NONE',  ( 0.000000000000000000, 1.000000000000000000, -4.956352788505160310E-16 ) ) ;
#15172=EDGE_CURVE ( 'NONE', #1922, #5666, #2405, .T. ) ;
#15176=CIRCLE ( 'NONE', #10918, 0.007874015748031516770 ) ;
#15181=ORIENTED_EDGE ( 'NONE', *, *, #53, .F. ) ;
#15189=DIRECTION ( 'NONE',  ( -0.000000000000000000, -1.000000000000000000, -0.000000000000000000 ) ) ;
#15193=DIRECTION ( 'NONE',  ( 0.000000000000000000, 1.000000000000000000, 0.000000000000000000 ) ) ;
#15198=CIRCLE ( 'NONE', #10724, 0.5905511811023621549 ) ;
#15205=CARTESIAN_POINT ( 'NONE',  ( 0.000000000000000000, 1.653543307086614567, 0.000000000000000000 ) ) ;
#15208=AXIS2_PLACEMENT_3D ( 'NONE', #1343, #6108, #9217 ) ;
#15212=DIRECTION ( 'NONE',  ( 0.000000000000000000, 0.000000000000000000, -1.000000000000000000 ) ) ;
#15214=LINE ( 'NONE', #4629, #220 ) ;
#15217=VERTEX_POINT ( 'NONE', #6018 ) ;
#15218=EDGE_CURVE ( 'NONE', #796, #4540, #12239, .T. ) ;
#15219=VERTEX_POINT ( 'NONE', #7279 ) ;
#15220=CIRCLE ( 'NONE', #9216, 0.6614173228346456046 ) ;
#15224=VECTOR ( 'NONE', #13400, 39.37007874015747433 ) ;
#15225=CARTESIAN_POINT ( 'NONE',  ( 0.000000000000000000, 1.645669291338583085, 0.000000000000000000 ) ) ;
#15226=DIRECTION ( 'NONE',  ( 0.8660254037844433705, 0.000000000000000000, 0.4999999999999918954 ) ) ;
#15234=VERTEX_POINT ( 'NONE', #6245 ) ;
#15241=ORIENTED_EDGE ( 'NONE', *, *, #14724, .T. ) ;
#15255=EDGE_CURVE ( 'NONE', #10823, #11092, #13465, .T. ) ;
#15259=FACE_OUTER_BOUND ( 'NONE', #5616, .T. ) ;
#15260=CARTESIAN_POINT ( 'NONE',  ( 0.000000000000000000, 1.346456692913385877, 0.000000000000000000 ) ) ;
#15263=DIRECTION ( 'NONE',  ( 0.000000000000000000, 0.000000000000000000, -1.000000000000000000 ) ) ;
#15270=VERTEX_POINT ( 'NONE', #11111 ) ;
#15271=EDGE_CURVE ( 'NONE', #2760, #6757, #6955, .T. ) ;
#15273=ADVANCED_FACE ( 'NONE', ( #401 ), #10458, .F. ) ;
#15275=DIRECTION ( 'NONE',  ( 0.000000000000000000, 1.000000000000000000, 0.000000000000000000 ) ) ;
#15277=DIRECTION ( 'NONE',  ( 0.000000000000000000, 0.000000000000000000, 1.000000000000000000 ) ) ;
#15282=EDGE_CURVE ( 'NONE', #10892, #11777, #10956, .T. ) ;
#15283=CARTESIAN_POINT ( 'NONE',  ( -0.05905511811023622659, 1.338626482899105241, -0.5946706712680680518 ) ) ;
#15291=PRODUCT_DEFINITION_SHAPE ( 'NONE', 'NONE',  #6282 ) ;
#15292=EDGE_LOOP ( 'NONE', ( #7730, #1498, #8276, #3192, #1584, #12571, #5621, #10640 ) ) ;
#15297=CARTESIAN_POINT ( 'NONE',  ( -0.5905511811023621549, 2.448818897637795367, -0.04724409448818898266 ) ) ;
#15307=ORIENTED_EDGE ( 'NONE', *, *, #11224, .T. ) ;
#15308=ADVANCED_BREP_SHAPE_REPRESENTATION ( '', ( #4199, #11481 ), #7464 ) ;
#15318=FACE_BOUND ( 'NONE', #2761, .T. ) ;
#15320=DIRECTION ( 'NONE',  ( -0.000000000000000000, -1.000000000000000000, -0.000000000000000000 ) ) ;
#15326=VERTEX_POINT ( 'NONE', #9775 ) ;
#15327=ORIENTED_EDGE ( 'NONE', *, *, #9619, .F. ) ;
#15330=DIRECTION ( 'NONE',  ( -0.000000000000000000, -1.000000000000000000, -0.000000000000000000 ) ) ;
#15334=CARTESIAN_POINT ( 'NONE',  ( 0.000000000000000000, 0.5905511811023621549, -0.7007874015748031260 ) ) ;
#15335=VECTOR ( 'NONE', #1475, 39.37007874015748143 ) ;
#15338=VERTEX_POINT ( 'NONE', #7186 ) ;
#15341=CARTESIAN_POINT ( 'NONE',  ( 6.846450609406462919E-17, 0.3464566929133857109, 0.5590551181102362266 ) ) ;
#15343=CIRCLE ( 'NONE', #9839, 0.007874015748031516770 ) ;
#15347=ORIENTED_EDGE ( 'NONE', *, *, #2078, .F. ) ;
#15352=ADVANCED_FACE ( 'NONE', ( #3740 ), #12274, .T. ) ;
#15358=EDGE_LOOP ( 'NONE', ( #14504, #9636, #8595, #1318 ) ) ;
#15359=CARTESIAN_POINT ( 'NONE',  ( 0.000000000000000000, 1.035433070866142113, 0.000000000000000000 ) ) ;
#15369=CIRCLE ( 'NONE', #14603, 0.6692913385826770867 ) ;
#15373=DIRECTION ( 'NONE',  ( 0.000000000000000000, 0.000000000000000000, -1.000000000000000000 ) ) ;
#15376=VECTOR ( 'NONE', #12951, 39.37007874015748143 ) ;
#15385=ORIENTED_EDGE ( 'NONE', *, *, #3755, .F. ) ;
#15387=DIRECTION ( 'NONE',  ( -0.8660254037844432595, 0.000000000000000000, -0.4999999999999918954 ) ) ;
#15388=CARTESIAN_POINT ( 'NONE',  ( 0.05905511811023622659, 1.043263280880422528, -0.5946706712680680518 ) ) ;
#15393=ORIENTED_EDGE ( 'NONE', *, *, #2809, .T. ) ;
#15395=VERTEX_POINT ( 'NONE', #1243 ) ;
#15396=VECTOR ( 'NONE', #3454, 39.37007874015748143 ) ;
#15397=ORIENTED_EDGE ( 'NONE', *, *, #12900, .T. ) ;
#15411=AXIS2_PLACEMENT_3D ( 'NONE', #2972, #12685, #13535 ) ;
#15415=CIRCLE ( 'NONE', #8651, 0.1653543307086614012 ) ;
#15420=EDGE_CURVE ( 'NONE', #13926, #5735, #2716, .T. ) ;
#15421=AXIS2_PLACEMENT_3D ( 'NONE', #12049, #3894, #121 ) ;
#15423=CARTESIAN_POINT ( 'NONE',  ( 0.000000000000000000, 0.000000000000000000, 0.000000000000000000 ) ) ;
#15425=FACE_OUTER_BOUND ( 'NONE', #6554, .T. ) ;
#15427=CARTESIAN_POINT ( 'NONE',  ( 0.05905511811023622659, 1.043307086614173373, -0.5952259495879739237 ) ) ;
#15428=EDGE_LOOP ( 'NONE', ( #5146, #1355, #12775, #812 ) ) ;
#15429=CARTESIAN_POINT ( 'NONE',  ( -0.1259842519685039353, 2.440944881889763884, -0.04724409448818898266 ) ) ;
#15433=ORIENTED_EDGE ( 'NONE', *, *, #13039, .T. ) ;
#15440=EDGE_CURVE ( 'NONE', #8101, #2525, #4723, .T. ) ;
#15443=DIRECTION ( 'NONE',  ( 0.000000000000000000, 1.000000000000000000, 0.000000000000000000 ) ) ;
#15445=ORIENTED_EDGE ( 'NONE', *, *, #4954, .F. ) ;
#15460=AXIS2_PLACEMENT_3D ( 'NONE', #9054, #7548, #523 ) ;
#15463=DIRECTION ( 'NONE',  ( -0.000000000000000000, -1.000000000000000000, -0.000000000000000000 ) ) ;
#15465=CARTESIAN_POINT ( 'NONE',  ( 0.000000000000000000, 0.04724409448818898960, -0.5433070866141731514 ) ) ;
#15466=CIRCLE ( 'NONE', #7201, 0.5905511811023621549 ) ;
#15469=CARTESIAN_POINT ( 'NONE',  ( 0.000000000000000000, 2.393700787401575436, 0.000000000000000000 ) ) ;
#15499=COLOUR_RGB('Dark Blue',0.08,0.2,0.34);
#15500=FILL_AREA_STYLE_COLOUR('',#15499);
#15501=FILL_AREA_STYLE('',(#15500));
#15502=SURFACE_STYLE_FILL_AREA(#15501);
#15503=SURFACE_SIDE_STYLE('',(#15502));
#15504=SURFACE_STYLE_USAGE(.BOTH.,#15503);
#15505=PRESENTATION_STYLE_ASSIGNMENT((#15504));
ENDSEC;
END-ISO-10303-21;
